ISO-10303-21;
HEADER;
FILE_DESCRIPTION (('STEP AP214'),
    '1' );
FILE_NAME ('MirrorHardened Serrated Safety Wedge.step',
    '2026-09-24T10:26:00',
    ( '' ),
    ( '' ),
    'SwSTEP 2.0',
    'SolidWorks 2026',
    '' );
FILE_SCHEMA (( 'AUTOMOTIVE_DESIGN' ));
ENDSEC;

DATA;
#2=DIRECTION ( 'NONE',  ( -1.000000000000000000, 0.000000000000000000, 0.000000000000000000 ) ) ;
#25=VERTEX_POINT ( 'NONE', #5412 ) ;
#30=ADVANCED_FACE ( 'NONE', ( #11114 ), #7526, .T. ) ;
#33=ORIENTED_EDGE ( 'NONE', *, *, #5062, .T. ) ;
#35=VECTOR ( 'NONE', #3157, 1000.000000000000000 ) ;
#43=DIRECTION ( 'NONE',  ( 0.000000000000000000, 1.000000000000000000, 0.000000000000000000 ) ) ;
#53=EDGE_CURVE ( 'NONE', #1573, #2995, #7662, .T. ) ;
#69=CARTESIAN_POINT ( 'NONE',  ( 22.00000000000000355, 30.00000000000000711, -25.00000000000000000 ) ) ;
#87=EDGE_LOOP ( 'NONE', ( #13526, #11711, #10761, #2317 ) ) ;
#95=ADVANCED_FACE ( 'NONE', ( #9801 ), #3380, .T. ) ;
#96=ADVANCED_FACE ( 'NONE', ( #3591 ), #13623, .F. ) ;
#98=DIRECTION ( 'NONE',  ( 0.000000000000000000, -1.000000000000000000, 0.000000000000000000 ) ) ;
#113=DIRECTION ( 'NONE',  ( 1.000000000000000000, 0.000000000000000000, -0.000000000000000000 ) ) ;
#120=CARTESIAN_POINT ( 'NONE',  ( 22.00000000000000355, 30.00000000000000711, -25.00000000000000000 ) ) ;
#127=ORIENTED_EDGE ( 'NONE', *, *, #5175, .F. ) ;
#128=ORIENTED_EDGE ( 'NONE', *, *, #2234, .F. ) ;
#134=DIRECTION ( 'NONE',  ( 0.000000000000000000, 0.000000000000000000, 1.000000000000000000 ) ) ;
#160=LINE ( 'NONE', #229, #1194 ) ;
#163=EDGE_CURVE ( 'NONE', #6145, #1954, #4682, .T. ) ;
#167=CARTESIAN_POINT ( 'NONE',  ( 0.000000000000000000, 0.000000000000000000, 0.000000000000000000 ) ) ;
#176=AXIS2_PLACEMENT_3D ( 'NONE', #8540, #7429, #5033 ) ;
#180=LINE ( 'NONE', #12266, #3484 ) ;
#199=VECTOR ( 'NONE', #5956, 1000.000000000000000 ) ;
#212=DIRECTION ( 'NONE',  ( 0.000000000000000000, 1.000000000000000000, 0.000000000000000000 ) ) ;
#222=DIRECTION ( 'NONE',  ( 1.000000000000000000, 0.000000000000000000, 0.000000000000000000 ) ) ;
#229=CARTESIAN_POINT ( 'NONE',  ( 24.99999999999999289, -4.898587196589414604E-15, -25.00000000000000000 ) ) ;
#230=EDGE_CURVE ( 'NONE', #2483, #11506, #8245, .T. ) ;
#261=LINE ( 'NONE', #9100, #14213 ) ;
#266=ORIENTED_EDGE ( 'NONE', *, *, #8071, .F. ) ;
#272=ORIENTED_EDGE ( 'NONE', *, *, #3606, .T. ) ;
#314=LINE ( 'NONE', #11495, #3240 ) ;
#339=DIRECTION ( 'NONE',  ( 1.000000000000000000, 0.000000000000000000, -0.000000000000000000 ) ) ;
#362=ORIENTED_EDGE ( 'NONE', *, *, #4420, .T. ) ;
#378=ORIENTED_EDGE ( 'NONE', *, *, #1938, .F. ) ;
#425=DIRECTION ( 'NONE',  ( 0.000000000000000000, -1.000000000000000000, 0.000000000000000000 ) ) ;
#428=ORIENTED_EDGE ( 'NONE', *, *, #9517, .T. ) ;
#484=ADVANCED_FACE ( 'NONE', ( #13027 ), #3077, .F. ) ;
#488=ORIENTED_EDGE ( 'NONE', *, *, #13152, .F. ) ;
#489=VECTOR ( 'NONE', #4311, 1000.000000000000000 ) ;
#498=CARTESIAN_POINT ( 'NONE',  ( 56.99999999999997868, -9.797174393178845379E-16, -25.00000000000000000 ) ) ;
#512=LINE ( 'NONE', #14249, #3944 ) ;
#520=ADVANCED_FACE ( 'NONE', ( #9180 ), #8896, .T. ) ;
#527=ORIENTED_EDGE ( 'NONE', *, *, #10032, .F. ) ;
#529=EDGE_LOOP ( 'NONE', ( #11917, #4776, #6144, #12759 ) ) ;
#535=VERTEX_POINT ( 'NONE', #5729 ) ;
#543=CARTESIAN_POINT ( 'NONE',  ( 30.10000000000000497, 29.99999999999999645, 6.999999999999992006 ) ) ;
#545=ORIENTED_EDGE ( 'NONE', *, *, #4939, .T. ) ;
#547=CARTESIAN_POINT ( 'NONE',  ( 22.00000000000000355, 27.00000000000000355, -25.00000000000000000 ) ) ;
#578=ORIENTED_EDGE ( 'NONE', *, *, #4864, .T. ) ;
#589=EDGE_CURVE ( 'NONE', #11502, #1350, #7940, .T. ) ;
#590=EDGE_LOOP ( 'NONE', ( #10183, #10627, #12842, #12199 ) ) ;
#606=VECTOR ( 'NONE', #3848, 1000.000000000000000 ) ;
#607=EDGE_CURVE ( 'NONE', #7346, #10278, #2254, .T. ) ;
#608=ORIENTED_EDGE ( 'NONE', *, *, #7283, .F. ) ;
#637=ORIENTED_EDGE ( 'NONE', *, *, #8722, .T. ) ;
#643=PLANE ( 'NONE',  #7331 ) ;
#659=ADVANCED_FACE ( 'NONE', ( #12942 ), #643, .F. ) ;
#669=AXIS2_PLACEMENT_3D ( 'NONE', #11683, #2851, #792 ) ;
#681=CARTESIAN_POINT ( 'NONE',  ( 22.00000000000000000, 60.00000000000000711, 25.00000000000000000 ) ) ;
#700=CARTESIAN_POINT ( 'NONE',  ( 22.00000000000000355, 40.00000000000000711, -25.00000000000000000 ) ) ;
#703=DIRECTION ( 'NONE',  ( 0.2425356250363328581, -0.9701425001453318764, -0.000000000000000000 ) ) ;
#706=DIRECTION ( 'NONE',  ( 0.000000000000000000, 0.000000000000000000, 1.000000000000000000 ) ) ;
#708=ORIENTED_EDGE ( 'NONE', *, *, #1688, .T. ) ;
#710=DIRECTION ( 'NONE',  ( 0.000000000000000000, 0.000000000000000000, -1.000000000000000000 ) ) ;
#747=EDGE_CURVE ( 'NONE', #10823, #25, #10507, .T. ) ;
#753=CARTESIAN_POINT ( 'NONE',  ( 56.99999999999997868, -9.797174393178845379E-16, -25.00000000000000000 ) ) ;
#760=CIRCLE ( 'NONE', #8929, 2.000000000000001776 ) ;
#765=ADVANCED_FACE ( 'NONE', ( #2762 ), #11597, .T. ) ;
#792=DIRECTION ( 'NONE',  ( -1.000000000000000000, 0.000000000000000000, 0.000000000000000000 ) ) ;
#800=DIRECTION ( 'NONE',  ( -1.000000000000000000, 0.000000000000000000, 0.000000000000000000 ) ) ;
#818=DIRECTION ( 'NONE',  ( 0.000000000000000000, 1.000000000000000000, 0.000000000000000000 ) ) ;
#849=ADVANCED_FACE ( 'NONE', ( #13081 ), #4374, .T. ) ;
#851=ORIENTED_EDGE ( 'NONE', *, *, #5392, .T. ) ;
#853=ORIENTED_EDGE ( 'NONE', *, *, #2264, .F. ) ;
#913=CARTESIAN_POINT ( 'NONE',  ( 20.00000000000000355, 17.00000000000000000, 25.00000000000000000 ) ) ;
#932=CARTESIAN_POINT ( 'NONE',  ( 22.00000000000000355, 40.00000000000000711, 25.00000000000000000 ) ) ;
#940=DIRECTION ( 'NONE',  ( 0.000000000000000000, 0.000000000000000000, -1.000000000000000000 ) ) ;
#950=VERTEX_POINT ( 'NONE', #13373 ) ;
#953=CONICAL_SURFACE ( 'NONE', #7496, 2.100000000000000977, 1.029744258676656754 ) ;
#973=ADVANCED_FACE ( 'NONE', ( #4450 ), #13506, .F. ) ;
#994=FILL_AREA_STYLE_COLOUR ( '', #8422 ) ;
#996=FACE_OUTER_BOUND ( 'NONE', #13697, .T. ) ;
#1000=VECTOR ( 'NONE', #6749, 1000.000000000000000 ) ;
#1005=ADVANCED_FACE ( 'NONE', ( #1202 ), #4715, .F. ) ;
#1009=DIRECTION ( 'NONE',  ( -1.000000000000000000, 0.000000000000000000, 0.000000000000000000 ) ) ;
#1013=CARTESIAN_POINT ( 'NONE',  ( 22.00000000000000000, 80.00000000000000000, -25.00000000000000000 ) ) ;
#1035=CYLINDRICAL_SURFACE ( 'NONE', #14302, 2.100000000000000977 ) ;
#1040=EDGE_CURVE ( 'NONE', #10278, #8394, #11429, .T. ) ;
#1043=CARTESIAN_POINT ( 'NONE',  ( 56.99999999999997868, -8.673617379884035472E-16, 25.00000000000000000 ) ) ;
#1046=CARTESIAN_POINT ( 'NONE',  ( 22.00000000000000000, 60.00000000000000711, -25.00000000000000000 ) ) ;
#1049=( NAMED_UNIT ( * ) PLANE_ANGLE_UNIT ( ) SI_UNIT ( $, .RADIAN. ) );
#1052=ORIENTED_EDGE ( 'NONE', *, *, #12586, .T. ) ;
#1056=CARTESIAN_POINT ( 'NONE',  ( 22.00000000000000711, 20.00000000000000355, 25.00000000000000000 ) ) ;
#1059=ADVANCED_FACE ( 'NONE', ( #1405 ), #5855, .T. ) ;
#1062=DIRECTION ( 'NONE',  ( 0.000000000000000000, 0.000000000000000000, 1.000000000000000000 ) ) ;
#1070=VECTOR ( 'NONE', #4923, 1000.000000000000000 ) ;
#1081=CARTESIAN_POINT ( 'NONE',  ( 57.35294117647057277, -1.411764705882362358, -25.00000000000000000 ) ) ;
#1084=VERTEX_POINT ( 'NONE', #12527 ) ;
#1085=DIRECTION ( 'NONE',  ( 0.000000000000000000, 0.000000000000000000, 1.000000000000000000 ) ) ;
#1111=VECTOR ( 'NONE', #7469, 1000.000000000000000 ) ;
#1119=CIRCLE ( 'NONE', #669, 2.100000000000000977 ) ;
#1123=VERTEX_POINT ( 'NONE', #13793 ) ;
#1129=CARTESIAN_POINT ( 'NONE',  ( 20.00000000000000000, -5.510910596163090344E-15, -25.00000000000000000 ) ) ;
#1130=DIRECTION ( 'NONE',  ( 1.000000000000000000, 1.224646799147353454E-16, 0.000000000000000000 ) ) ;
#1135=LINE ( 'NONE', #3419, #8609 ) ;
#1142=DIRECTION ( 'NONE',  ( -0.9701425001453319874, -0.2425356250363328858, 0.000000000000000000 ) ) ;
#1143=AXIS2_PLACEMENT_3D ( 'NONE', #11118, #5746, #2 ) ;
#1148=CARTESIAN_POINT ( 'NONE',  ( 19.99999999999999645, 57.00000000000000000, -25.00000000000000000 ) ) ;
#1150=PLANE ( 'NONE',  #3266 ) ;
#1186=DIRECTION ( 'NONE',  ( 0.000000000000000000, 0.000000000000000000, 1.000000000000000000 ) ) ;
#1194=VECTOR ( 'NONE', #1542, 1000.000000000000000 ) ;
#1202=FACE_OUTER_BOUND ( 'NONE', #4837, .T. ) ;
#1220=CARTESIAN_POINT ( 'NONE',  ( 22.00000000000000355, 40.00000000000000711, -25.00000000000000000 ) ) ;
#1231=DIRECTION ( 'NONE',  ( -0.000000000000000000, -0.000000000000000000, -1.000000000000000000 ) ) ;
#1244=EDGE_CURVE ( 'NONE', #5199, #9008, #14226, .T. ) ;
#1250=DIRECTION ( 'NONE',  ( -1.000000000000000000, 0.000000000000000000, 0.000000000000000000 ) ) ;
#1253=CARTESIAN_POINT ( 'NONE',  ( 22.00000000000000355, 47.00000000000000000, -25.00000000000000000 ) ) ;
#1260=DIRECTION ( 'NONE',  ( -1.000000000000000000, 0.000000000000000000, 0.000000000000000000 ) ) ;
#1267=VECTOR ( 'NONE', #2666, 1000.000000000000000 ) ;
#1273=LINE ( 'NONE', #5448, #10327 ) ;
#1277=CARTESIAN_POINT ( 'NONE',  ( 28.00000000000000355, 29.99999999999999645, 5.738192700042120897 ) ) ;
#1278=CARTESIAN_POINT ( 'NONE',  ( 53.99999999999997868, -1.324077043022348342E-15, 25.00000000000000000 ) ) ;
#1281=DIRECTION ( 'NONE',  ( -1.000000000000000000, 0.000000000000000000, 0.000000000000000000 ) ) ;
#1309=ORIENTED_EDGE ( 'NONE', *, *, #7633, .T. ) ;
#1327=CARTESIAN_POINT ( 'NONE',  ( 20.00000000000000000, -5.510910596163090344E-15, -25.00000000000000000 ) ) ;
#1340=LINE ( 'NONE', #3421, #10474 ) ;
#1347=ORIENTED_EDGE ( 'NONE', *, *, #10810, .F. ) ;
#1350=VERTEX_POINT ( 'NONE', #8149 ) ;
#1352=VERTEX_POINT ( 'NONE', #9484 ) ;
#1363=EDGE_CURVE ( 'NONE', #25, #4424, #4943, .T. ) ;
#1367=VECTOR ( 'NONE', #13668, 1000.000000000000000 ) ;
#1401=CARTESIAN_POINT ( 'NONE',  ( 20.00000000000000000, 80.00000000000000000, -25.00000000000000000 ) ) ;
#1403=ADVANCED_FACE ( 'NONE', ( #12851 ), #8223, .F. ) ;
#1405=FACE_OUTER_BOUND ( 'NONE', #10834, .T. ) ;
#1410=VECTOR ( 'NONE', #8000, 1000.000000000000000 ) ;
#1414=AXIS2_PLACEMENT_3D ( 'NONE', #6975, #339, #10579 ) ;
#1430=ORIENTED_EDGE ( 'NONE', *, *, #6494, .T. ) ;
#1437=VECTOR ( 'NONE', #9792, 1000.000000000000000 ) ;
#1444=DIRECTION ( 'NONE',  ( 0.000000000000000000, 1.000000000000000000, 0.000000000000000000 ) ) ;
#1448=VECTOR ( 'NONE', #12943, 1000.000000000000000 ) ;
#1455=ORIENTED_EDGE ( 'NONE', *, *, #13368, .T. ) ;
#1460=LINE ( 'NONE', #3520, #8902 ) ;
#1470=LINE ( 'NONE', #8188, #12661 ) ;
#1494=FACE_OUTER_BOUND ( 'NONE', #3379, .T. ) ;
#1497=AXIS2_PLACEMENT_3D ( 'NONE', #1574, #6026, #7203 ) ;
#1512=AXIS2_PLACEMENT_3D ( 'NONE', #4552, #6998, #4613 ) ;
#1516=LINE ( 'NONE', #5029, #199 ) ;
#1530=LINE ( 'NONE', #11553, #8631 ) ;
#1539=ORIENTED_EDGE ( 'NONE', *, *, #4420, .F. ) ;
#1542=DIRECTION ( 'NONE',  ( 0.000000000000000000, 0.000000000000000000, 1.000000000000000000 ) ) ;
#1545=VERTEX_POINT ( 'NONE', #1043 ) ;
#1546=EDGE_CURVE ( 'NONE', #1084, #8394, #9968, .T. ) ;
#1553=DIRECTION ( 'NONE',  ( 0.000000000000000000, 1.000000000000000000, 0.000000000000000000 ) ) ;
#1554=LINE ( 'NONE', #11653, #1070 ) ;
#1559=DIRECTION ( 'NONE',  ( 0.000000000000000000, 0.000000000000000000, 1.000000000000000000 ) ) ;
#1570=EDGE_LOOP ( 'NONE', ( #11826, #4173, #11309, #4560 ) ) ;
#1573=VERTEX_POINT ( 'NONE', #12516 ) ;
#1574=CARTESIAN_POINT ( 'NONE',  ( 22.00000000000000355, 50.00000000000000000, -25.00000000000000000 ) ) ;
#1577=VERTEX_POINT ( 'NONE', #9147 ) ;
#1605=CARTESIAN_POINT ( 'NONE',  ( 20.00000000000000355, 30.00000000000000711, 25.00000000000000000 ) ) ;
#1612=EDGE_CURVE ( 'NONE', #11488, #1123, #160, .T. ) ;
#1626=VECTOR ( 'NONE', #3990, 1000.000000000000000 ) ;
#1628=UNCERTAINTY_MEASURE_WITH_UNIT (LENGTH_MEASURE( 1.000000000000000082E-05 ), #6520, 'distance_accuracy_value', 'NONE');
#1633=ADVANCED_FACE ( 'NONE', ( #7019 ), #2652, .T. ) ;
#1655=CARTESIAN_POINT ( 'NONE',  ( 22.00000000000000000, 70.00000000000000000, 25.00000000000000000 ) ) ;
#1658=CARTESIAN_POINT ( 'NONE',  ( 22.00000000000000355, 47.00000000000000000, -25.00000000000000000 ) ) ;
#1672=ORIENTED_EDGE ( 'NONE', *, *, #3743, .T. ) ;
#1687=VECTOR ( 'NONE', #1130, 1000.000000000000000 ) ;
#1688=EDGE_CURVE ( 'NONE', #3669, #13670, #9002, .T. ) ;
#1696=EDGE_CURVE ( 'NONE', #10936, #1577, #14075, .T. ) ;
#1706=ORIENTED_EDGE ( 'NONE', *, *, #4939, .F. ) ;
#1710=ORIENTED_EDGE ( 'NONE', *, *, #5542, .T. ) ;
#1736=DIRECTION ( 'NONE',  ( 0.000000000000000000, 0.000000000000000000, 1.000000000000000000 ) ) ;
#1753=VERTEX_POINT ( 'NONE', #14148 ) ;
#1764=ORIENTED_EDGE ( 'NONE', *, *, #163, .T. ) ;
#1772=VERTEX_POINT ( 'NONE', #1774 ) ;
#1774=CARTESIAN_POINT ( 'NONE',  ( 20.00000000000000000, 5.000000000000000000, 25.00000000000000000 ) ) ;
#1811=CARTESIAN_POINT ( 'NONE',  ( 20.00000000000000711, 20.00000000000000355, 25.00000000000000000 ) ) ;
#1830=AXIS2_PLACEMENT_3D ( 'NONE', #2192, #4329, #1009 ) ;
#1831=DIRECTION ( 'NONE',  ( 0.000000000000000000, 1.000000000000000000, 0.000000000000000000 ) ) ;
#1838=EDGE_CURVE ( 'NONE', #9244, #1753, #14425, .T. ) ;
#1845=AXIS2_PLACEMENT_3D ( 'NONE', #9928, #1142, #13382 ) ;
#1847=ORIENTED_EDGE ( 'NONE', *, *, #12373, .T. ) ;
#1853=ORIENTED_EDGE ( 'NONE', *, *, #13064, .T. ) ;
#1862=PLANE ( 'NONE',  #12207 ) ;
#1874=EDGE_LOOP ( 'NONE', ( #2929, #7336, #11493, #6111 ) ) ;
#1875=ORIENTED_EDGE ( 'NONE', *, *, #12362, .T. ) ;
#1877=CARTESIAN_POINT ( 'NONE',  ( 28.00000000000000355, 29.99999999999999645, 25.00000000000000000 ) ) ;
#1882=CARTESIAN_POINT ( 'NONE',  ( 20.00000000000000000, -5.510910596163090344E-15, -25.00000000000000000 ) ) ;
#1896=CARTESIAN_POINT ( 'NONE',  ( 22.00000000000000000, 57.00000000000000000, -25.00000000000000000 ) ) ;
#1901=CARTESIAN_POINT ( 'NONE',  ( 25.90000000000000213, 29.99999999999999645, 6.999999999999992006 ) ) ;
#1906=DIRECTION ( 'NONE',  ( 1.000000000000000000, 0.000000000000000000, 0.000000000000000000 ) ) ;
#1908=LINE ( 'NONE', #3092, #14326 ) ;
#1938=EDGE_CURVE ( 'NONE', #950, #13670, #9058, .T. ) ;
#1950=ORIENTED_EDGE ( 'NONE', *, *, #53, .F. ) ;
#1954=VERTEX_POINT ( 'NONE', #4820 ) ;
#1981=ORIENTED_EDGE ( 'NONE', *, *, #7232, .F. ) ;
#2000=CARTESIAN_POINT ( 'NONE',  ( 20.00000000000000000, -5.510910596163090344E-15, -25.00000000000000000 ) ) ;
#2006=CARTESIAN_POINT ( 'NONE',  ( 20.00000000000000711, 20.00000000000000355, -25.00000000000000000 ) ) ;
#2015=ORIENTED_EDGE ( 'NONE', *, *, #9070, .F. ) ;
#2018=DIRECTION ( 'NONE',  ( -1.000000000000000000, 0.000000000000000000, 0.000000000000000000 ) ) ;
#2019=DIRECTION ( 'NONE',  ( 1.000000000000000000, 0.000000000000000000, 0.000000000000000000 ) ) ;
#2040=SHAPE_DEFINITION_REPRESENTATION ( #4978, #4344 ) ;
#2063=DIRECTION ( 'NONE',  ( -0.2425356250363328581, 0.9701425001453318764, 0.000000000000000000 ) ) ;
#2072=CARTESIAN_POINT ( 'NONE',  ( 36.99999999999999289, 80.00000000000000000, -25.00000000000000000 ) ) ;
#2074=PRESENTATION_STYLE_ASSIGNMENT (( #13069 ) ) ;
#2076=DIRECTION ( 'NONE',  ( 0.000000000000000000, 0.000000000000000000, -1.000000000000000000 ) ) ;
#2086=VERTEX_POINT ( 'NONE', #13840 ) ;
#2125=ORIENTED_EDGE ( 'NONE', *, *, #11328, .F. ) ;
#2128=CARTESIAN_POINT ( 'NONE',  ( 57.35294117647057277, -1.411764705882362358, 25.00000000000000000 ) ) ;
#2129=CARTESIAN_POINT ( 'NONE',  ( 30.10000000000000497, 29.99999999999999645, 25.00000000000000000 ) ) ;
#2131=ORIENTED_EDGE ( 'NONE', *, *, #3606, .F. ) ;
#2167=DIRECTION ( 'NONE',  ( 0.000000000000000000, 0.000000000000000000, 1.000000000000000000 ) ) ;
#2169=CARTESIAN_POINT ( 'NONE',  ( 22.00000000000000000, 78.00000000000000000, -25.00000000000000000 ) ) ;
#2192=CARTESIAN_POINT ( 'NONE',  ( 28.00000000000000355, 29.99999999999999645, 6.999999999999992006 ) ) ;
#2199=CARTESIAN_POINT ( 'NONE',  ( 33.99999999999998579, 80.00000000000000000, -23.00000000000000000 ) ) ;
#2201=EDGE_LOOP ( 'NONE', ( #2271, #6042, #266, #5597 ) ) ;
#2217=ORIENTED_EDGE ( 'NONE', *, *, #13988, .T. ) ;
#2221=CARTESIAN_POINT ( 'NONE',  ( 20.00000000000000000, -5.510910596163090344E-15, 25.00000000000000000 ) ) ;
#2222=EDGE_CURVE ( 'NONE', #8618, #6890, #10004, .T. ) ;
#2228=VERTEX_POINT ( 'NONE', #6632 ) ;
#2234=EDGE_CURVE ( 'NONE', #5517, #6626, #9936, .T. ) ;
#2254=LINE ( 'NONE', #1220, #4100 ) ;
#2261=DIRECTION ( 'NONE',  ( 0.9701425001453319874, 0.2425356250363328858, 0.000000000000000000 ) ) ;
#2263=CARTESIAN_POINT ( 'NONE',  ( 22.00000000000000355, 40.00000000000000711, -25.00000000000000000 ) ) ;
#2264=EDGE_CURVE ( 'NONE', #535, #4153, #3287, .T. ) ;
#2271=ORIENTED_EDGE ( 'NONE', *, *, #6202, .T. ) ;
#2294=EDGE_CURVE ( 'NONE', #2086, #13783, #9869, .T. ) ;
#2295=ORIENTED_EDGE ( 'NONE', *, *, #13368, .F. ) ;
#2312=EDGE_CURVE ( 'NONE', #6145, #3032, #9788, .T. ) ;
#2317=ORIENTED_EDGE ( 'NONE', *, *, #11197, .F. ) ;
#2326=CARTESIAN_POINT ( 'NONE',  ( 60.00000000000000000, -6.123233995736768255E-16, -25.00000000000000000 ) ) ;
#2331=VECTOR ( 'NONE', #11780, 1000.000000000000000 ) ;
#2339=ADVANCED_FACE ( 'NONE', ( #7581, #14338 ), #1150, .T. ) ;
#2342=CARTESIAN_POINT ( 'NONE',  ( 0.000000000000000000, 0.000000000000000000, -25.00000000000000000 ) ) ;
#2440=EDGE_LOOP ( 'NONE', ( #7449, #6177, #2217, #11767 ) ) ;
#2454=CARTESIAN_POINT ( 'NONE',  ( 60.00000000000000000, -6.123233995736768255E-16, -25.00000000000000000 ) ) ;
#2469=ORIENTED_EDGE ( 'NONE', *, *, #2475, .F. ) ;
#2475=EDGE_CURVE ( 'NONE', #3711, #3862, #12776, .T. ) ;
#2483=VERTEX_POINT ( 'NONE', #1658 ) ;
#2526=ORIENTED_EDGE ( 'NONE', *, *, #4864, .F. ) ;
#2530=VECTOR ( 'NONE', #13377, 1000.000000000000000 ) ;
#2535=ORIENTED_EDGE ( 'NONE', *, *, #13933, .F. ) ;
#2545=AXIS2_PLACEMENT_3D ( 'NONE', #1882, #12860, #5093 ) ;
#2569=ORIENTED_EDGE ( 'NONE', *, *, #2575, .F. ) ;
#2575=EDGE_CURVE ( 'NONE', #9662, #6876, #5453, .T. ) ;
#2612=CARTESIAN_POINT ( 'NONE',  ( 19.99999999999999645, 57.00000000000000000, 25.00000000000000000 ) ) ;
#2640=DIRECTION ( 'NONE',  ( 0.000000000000000000, 0.000000000000000000, 1.000000000000000000 ) ) ;
#2652=PLANE ( 'NONE',  #13136 ) ;
#2666=DIRECTION ( 'NONE',  ( -1.000000000000000000, 0.000000000000000000, 0.000000000000000000 ) ) ;
#2667=CARTESIAN_POINT ( 'NONE',  ( 22.00000000000000000, 57.00000000000000000, 25.00000000000000000 ) ) ;
#2668=ORIENTED_EDGE ( 'NONE', *, *, #9947, .T. ) ;
#2681=CARTESIAN_POINT ( 'NONE',  ( 22.00000000000000355, 27.00000000000000355, -25.00000000000000000 ) ) ;
#2700=DIRECTION ( 'NONE',  ( -0.000000000000000000, -1.000000000000000000, 0.000000000000000000 ) ) ;
#2732=PLANE ( 'NONE',  #6481 ) ;
#2743=ORIENTED_EDGE ( 'NONE', *, *, #9653, .T. ) ;
#2751=ORIENTED_EDGE ( 'NONE', *, *, #1688, .F. ) ;
#2762=FACE_OUTER_BOUND ( 'NONE', #590, .T. ) ;
#2806=VERTEX_POINT ( 'NONE', #1277 ) ;
#2836=EDGE_CURVE ( 'NONE', #3862, #4403, #180, .T. ) ;
#2851=DIRECTION ( 'NONE',  ( 0.000000000000000000, 0.000000000000000000, -1.000000000000000000 ) ) ;
#2854=VECTOR ( 'NONE', #5767, 1000.000000000000000 ) ;
#2855=EDGE_CURVE ( 'NONE', #13646, #10382, #1135, .T. ) ;
#2889=ORIENTED_EDGE ( 'NONE', *, *, #12977, .F. ) ;
#2911=EDGE_LOOP ( 'NONE', ( #1875, #5174, #1539, #8169, #12998, #8548, #4295, #10199, #7142, #14194, #2469, #11280, #6522, #3009, #10776, #6460, #9470, #2889, #1950, #8452, #1981, #14109, #488, #9956, #9578, #6218, #9252, #2743, #11084, #4109 ) ) ;
#2920=CARTESIAN_POINT ( 'NONE',  ( 20.00000000000000355, 17.00000000000000000, -25.00000000000000000 ) ) ;
#2926=EDGE_CURVE ( 'NONE', #8962, #3669, #9391, .T. ) ;
#2929=ORIENTED_EDGE ( 'NONE', *, *, #10810, .T. ) ;
#2937=ORIENTED_EDGE ( 'NONE', *, *, #8949, .F. ) ;
#2942=CARTESIAN_POINT ( 'NONE',  ( 28.00000000000000355, 29.99999999999999645, 6.999999999999992006 ) ) ;
#2955=ORIENTED_EDGE ( 'NONE', *, *, #13772, .T. ) ;
#2976=ADVANCED_FACE ( 'NONE', ( #1494 ), #7111, .F. ) ;
#2980=ORIENTED_EDGE ( 'NONE', *, *, #10911, .T. ) ;
#2995=VERTEX_POINT ( 'NONE', #13417 ) ;
#2999=DIRECTION ( 'NONE',  ( 0.000000000000000000, 0.000000000000000000, 1.000000000000000000 ) ) ;
#3004=ORIENTED_EDGE ( 'NONE', *, *, #3700, .F. ) ;
#3006=DIRECTION ( 'NONE',  ( 0.7071067811865483499, 0.7071067811865467956, -0.000000000000000000 ) ) ;
#3007=ORIENTED_EDGE ( 'NONE', *, *, #10626, .F. ) ;
#3009=ORIENTED_EDGE ( 'NONE', *, *, #12007, .F. ) ;
#3032=VERTEX_POINT ( 'NONE', #13257 ) ;
#3077=PLANE ( 'NONE',  #3142 ) ;
#3079=ORIENTED_EDGE ( 'NONE', *, *, #3769, .F. ) ;
#3086=LINE ( 'NONE', #5048, #14071 ) ;
#3092=CARTESIAN_POINT ( 'NONE',  ( 22.00000000000000355, 30.00000000000000711, 25.00000000000000000 ) ) ;
#3097=VERTEX_POINT ( 'NONE', #8992 ) ;
#3098=DIRECTION ( 'NONE',  ( 0.000000000000000000, 0.000000000000000000, -1.000000000000000000 ) ) ;
#3101=VECTOR ( 'NONE', #1062, 1000.000000000000000 ) ;
#3102=ORIENTED_EDGE ( 'NONE', *, *, #10316, .T. ) ;
#3109=ADVANCED_FACE ( 'NONE', ( #12370 ), #6800, .F. ) ;
#3114=DIRECTION ( 'NONE',  ( 0.000000000000000000, 0.000000000000000000, 1.000000000000000000 ) ) ;
#3117=CARTESIAN_POINT ( 'NONE',  ( 36.99999999999999289, 80.00000000000000000, 25.00000000000000000 ) ) ;
#3132=CARTESIAN_POINT ( 'NONE',  ( 22.00000000000000000, 60.00000000000000711, -25.00000000000000000 ) ) ;
#3141=SURFACE_STYLE_FILL_AREA ( #4240 ) ;
#3142=AXIS2_PLACEMENT_3D ( 'NONE', #6413, #3006, #7436 ) ;
#3147=ORIENTED_EDGE ( 'NONE', *, *, #14087, .T. ) ;
#3157=DIRECTION ( 'NONE',  ( -0.000000000000000000, -1.000000000000000000, 0.000000000000000000 ) ) ;
#3182=LINE ( 'NONE', #6311, #1111 ) ;
#3196=LINE ( 'NONE', #11906, #12910 ) ;
#3198=CARTESIAN_POINT ( 'NONE',  ( 22.00000000000000000, 70.00000000000000000, -25.00000000000000000 ) ) ;
#3204=CARTESIAN_POINT ( 'NONE',  ( 57.35294117647057277, -1.411764705882362358, -23.00000000000000000 ) ) ;
#3217=LINE ( 'NONE', #4470, #10464 ) ;
#3230=PLANE ( 'NONE',  #3954 ) ;
#3240=VECTOR ( 'NONE', #7916, 1000.000000000000114 ) ;
#3242=LINE ( 'NONE', #13202, #3805 ) ;
#3255=VERTEX_POINT ( 'NONE', #8652 ) ;
#3259=CARTESIAN_POINT ( 'NONE',  ( 20.00000000000000000, -5.510910596163090344E-15, -25.00000000000000000 ) ) ;
#3264=ORIENTED_EDGE ( 'NONE', *, *, #9653, .F. ) ;
#3266=AXIS2_PLACEMENT_3D ( 'NONE', #6986, #8974, #5731 ) ;
#3269=DIRECTION ( 'NONE',  ( 0.000000000000000000, 0.000000000000000000, 1.000000000000000000 ) ) ;
#3287=LINE ( 'NONE', #8693, #6049 ) ;
#3290=CARTESIAN_POINT ( 'NONE',  ( 20.00000000000000000, 27.00000000000000355, 25.00000000000000000 ) ) ;
#3301=DIRECTION ( 'NONE',  ( 0.000000000000000000, 0.000000000000000000, 1.000000000000000000 ) ) ;
#3333=CARTESIAN_POINT ( 'NONE',  ( 22.00000000000000711, 17.00000000000000000, 25.00000000000000000 ) ) ;
#3372=ORIENTED_EDGE ( 'NONE', *, *, #4152, .F. ) ;
#3379=EDGE_LOOP ( 'NONE', ( #11741, #8124, #10747, #2937 ) ) ;
#3380=PLANE ( 'NONE',  #13677 ) ;
#3395=DIRECTION ( 'NONE',  ( 0.000000000000000000, 0.000000000000000000, 1.000000000000000000 ) ) ;
#3410=ORIENTED_EDGE ( 'NONE', *, *, #2855, .T. ) ;
#3417=LINE ( 'NONE', #6613, #4635 ) ;
#3419=CARTESIAN_POINT ( 'NONE',  ( 22.00000000000000355, 30.00000000000000711, -25.00000000000000000 ) ) ;
#3421=CARTESIAN_POINT ( 'NONE',  ( 20.00000000000000000, -5.510910596163090344E-15, 25.00000000000000000 ) ) ;
#3423=PLANE ( 'NONE',  #1845 ) ;
#3432=EDGE_CURVE ( 'NONE', #1577, #3032, #8227, .T. ) ;
#3442=VERTEX_POINT ( 'NONE', #8378 ) ;
#3446=ORIENTED_EDGE ( 'NONE', *, *, #2836, .T. ) ;
#3465=CARTESIAN_POINT ( 'NONE',  ( 22.00000000000000355, 30.00000000000000711, -25.00000000000000000 ) ) ;
#3467=LINE ( 'NONE', #7913, #13790 ) ;
#3484=VECTOR ( 'NONE', #4651, 1000.000000000000000 ) ;
#3489=CARTESIAN_POINT ( 'NONE',  ( 20.00000000000000000, -5.510910596163090344E-15, -25.00000000000000000 ) ) ;
#3512=VECTOR ( 'NONE', #12965, 1000.000000000000000 ) ;
#3520=CARTESIAN_POINT ( 'NONE',  ( 20.00000000000000000, -5.510910596163090344E-15, -25.00000000000000000 ) ) ;
#3547=VECTOR ( 'NONE', #12816, 1000.000000000000000 ) ;
#3556=AXIS2_PLACEMENT_3D ( 'NONE', #8487, #12973, #4041 ) ;
#3562=EDGE_CURVE ( 'NONE', #12012, #5916, #11978, .T. ) ;
#3563=DIRECTION ( 'NONE',  ( 1.000000000000000000, 0.000000000000000000, -0.000000000000000000 ) ) ;
#3565=EDGE_CURVE ( 'NONE', #11502, #1577, #3196, .T. ) ;
#3570=VECTOR ( 'NONE', #2076, 1000.000000000000000 ) ;
#3581=EDGE_CURVE ( 'NONE', #1352, #1753, #6581, .T. ) ;
#3591=FACE_OUTER_BOUND ( 'NONE', #9575, .T. ) ;
#3593=ORIENTED_EDGE ( 'NONE', *, *, #12373, .F. ) ;
#3599=EDGE_CURVE ( 'NONE', #12012, #3255, #7562, .T. ) ;
#3606=EDGE_CURVE ( 'NONE', #5482, #9930, #10659, .T. ) ;
#3607=AXIS2_PLACEMENT_3D ( 'NONE', #5651, #113, #9088 ) ;
#3614=ORIENTED_EDGE ( 'NONE', *, *, #11485, .T. ) ;
#3620=DIRECTION ( 'NONE',  ( -0.7071067811865467956, 0.7071067811865483499, 0.000000000000000000 ) ) ;
#3635=ORIENTED_EDGE ( 'NONE', *, *, #8949, .T. ) ;
#3669=VERTEX_POINT ( 'NONE', #11004 ) ;
#3687=UNCERTAINTY_MEASURE_WITH_UNIT (LENGTH_MEASURE( 1.000000000000000082E-05 ), #4854, 'distance_accuracy_value', 'NONE');
#3689=DIRECTION ( 'NONE',  ( 0.7071067811865467956, -0.7071067811865483499, -0.000000000000000000 ) ) ;
#3700=EDGE_CURVE ( 'NONE', #7329, #1352, #6685, .T. ) ;
#3707=EDGE_CURVE ( 'NONE', #2228, #8962, #5652, .T. ) ;
#3711=VERTEX_POINT ( 'NONE', #4520 ) ;
#3732=VECTOR ( 'NONE', #8761, 1000.000000000000000 ) ;
#3743=EDGE_CURVE ( 'NONE', #11965, #11358, #1273, .T. ) ;
#3745=VECTOR ( 'NONE', #14215, 1000.000000000000000 ) ;
#3769=EDGE_CURVE ( 'NONE', #2806, #9244, #12528, .T. ) ;
#3792=DIRECTION ( 'NONE',  ( 1.000000000000000000, 0.000000000000000000, 0.000000000000000000 ) ) ;
#3800=EDGE_CURVE ( 'NONE', #12392, #11488, #4783, .T. ) ;
#3805=VECTOR ( 'NONE', #8931, 1000.000000000000000 ) ;
#3831=VECTOR ( 'NONE', #3620, 1000.000000000000000 ) ;
#3839=ORIENTED_EDGE ( 'NONE', *, *, #1363, .T. ) ;
#3844=CARTESIAN_POINT ( 'NONE',  ( 20.00000000000000355, 40.00000000000000711, 25.00000000000000000 ) ) ;
#3848=DIRECTION ( 'NONE',  ( 0.000000000000000000, 0.000000000000000000, 1.000000000000000000 ) ) ;
#3855=DIRECTION ( 'NONE',  ( 0.000000000000000000, 0.000000000000000000, 1.000000000000000000 ) ) ;
#3862=VERTEX_POINT ( 'NONE', #2667 ) ;
#3868=CARTESIAN_POINT ( 'NONE',  ( 20.00000000000000355, 30.00000000000000711, -25.00000000000000000 ) ) ;
#3876=EDGE_CURVE ( 'NONE', #7437, #8618, #1554, .T. ) ;
#3895=DIRECTION ( 'NONE',  ( 0.000000000000000000, -1.000000000000000000, 0.000000000000000000 ) ) ;
#3915=LINE ( 'NONE', #13800, #12568 ) ;
#3944=VECTOR ( 'NONE', #11620, 1000.000000000000000 ) ;
#3950=EDGE_LOOP ( 'NONE', ( #1847, #1853, #9279, #11449 ) ) ;
#3954=AXIS2_PLACEMENT_3D ( 'NONE', #12297, #11332, #5619 ) ;
#3964=LINE ( 'NONE', #13111, #35 ) ;
#3977=DIRECTION ( 'NONE',  ( 0.000000000000000000, -1.000000000000000000, 0.000000000000000000 ) ) ;
#3980=LINE ( 'NONE', #9814, #13415 ) ;
#3990=DIRECTION ( 'NONE',  ( 1.000000000000000000, 1.224646799147353454E-16, 0.000000000000000000 ) ) ;
#3996=VECTOR ( 'NONE', #8356, 1000.000000000000000 ) ;
#4000=FACE_OUTER_BOUND ( 'NONE', #6541, .T. ) ;
#4028=AXIS2_PLACEMENT_3D ( 'NONE', #1081, #2261, #11252 ) ;
#4031=CARTESIAN_POINT ( 'NONE',  ( 20.00000000000000355, 40.00000000000000711, -25.00000000000000000 ) ) ;
#4033=VECTOR ( 'NONE', #13846, 1000.000000000000000 ) ;
#4041=DIRECTION ( 'NONE',  ( -1.000000000000000000, 0.000000000000000000, 0.000000000000000000 ) ) ;
#4048=DIRECTION ( 'NONE',  ( 0.000000000000000000, 0.000000000000000000, 1.000000000000000000 ) ) ;
#4061=DIRECTION ( 'NONE',  ( 0.000000000000000000, 0.000000000000000000, 1.000000000000000000 ) ) ;
#4066=ORIENTED_EDGE ( 'NONE', *, *, #1363, .F. ) ;
#4100=VECTOR ( 'NONE', #6698, 1000.000000000000000 ) ;
#4104=VERTEX_POINT ( 'NONE', #8936 ) ;
#4106=PLANE ( 'NONE',  #176 ) ;
#4109=ORIENTED_EDGE ( 'NONE', *, *, #7683, .T. ) ;
#4110=ORIENTED_EDGE ( 'NONE', *, *, #9395, .T. ) ;
#4114=ORIENTED_EDGE ( 'NONE', *, *, #11328, .T. ) ;
#4146=DIRECTION ( 'NONE',  ( -1.000000000000000000, 0.000000000000000000, 0.000000000000000000 ) ) ;
#4152=EDGE_CURVE ( 'NONE', #13612, #1573, #12094, .T. ) ;
#4153=VERTEX_POINT ( 'NONE', #1046 ) ;
#4160=DIRECTION ( 'NONE',  ( 1.000000000000000000, 0.000000000000000000, 0.000000000000000000 ) ) ;
#4161=ORIENTED_EDGE ( 'NONE', *, *, #5552, .T. ) ;
#4173=ORIENTED_EDGE ( 'NONE', *, *, #3565, .T. ) ;
#4183=LINE ( 'NONE', #4260, #13140 ) ;
#4186=LINE ( 'NONE', #8628, #8199 ) ;
#4190=DIRECTION ( 'NONE',  ( -1.000000000000000000, 0.000000000000000000, 0.000000000000000000 ) ) ;
#4196=CARTESIAN_POINT ( 'NONE',  ( 22.00000000000000000, 78.00000000000000000, 25.00000000000000000 ) ) ;
#4203=EDGE_LOOP ( 'NONE', ( #1706, #10875, #1309, #3007 ) ) ;
#4217=VERTEX_POINT ( 'NONE', #8192 ) ;
#4229=ORIENTED_EDGE ( 'NONE', *, *, #9530, .T. ) ;
#4231=DIRECTION ( 'NONE',  ( -1.000000000000000000, 0.000000000000000000, 0.000000000000000000 ) ) ;
#4240=FILL_AREA_STYLE ('',( #994 ) ) ;
#4245=ORIENTED_EDGE ( 'NONE', *, *, #13402, .T. ) ;
#4251=EDGE_LOOP ( 'NONE', ( #11878, #7206, #5369, #10185 ) ) ;
#4260=CARTESIAN_POINT ( 'NONE',  ( 20.00000000000000000, 80.00000000000000000, 25.00000000000000000 ) ) ;
#4262=LINE ( 'NONE', #4569, #10065 ) ;
#4285=ADVANCED_FACE ( 'NONE', ( #9370 ), #13853, .T. ) ;
#4292=CARTESIAN_POINT ( 'NONE',  ( 20.00000000000000000, 60.00000000000000711, -25.00000000000000000 ) ) ;
#4295=ORIENTED_EDGE ( 'NONE', *, *, #3565, .F. ) ;
#4311=DIRECTION ( 'NONE',  ( 0.000000000000000000, 1.000000000000000000, 0.000000000000000000 ) ) ;
#4314=DIRECTION ( 'NONE',  ( 0.000000000000000000, 0.000000000000000000, -1.000000000000000000 ) ) ;
#4316=EDGE_LOOP ( 'NONE', ( #12514, #13905, #3614, #4526, #7504, #7579, #8296, #13590, #5021, #4981, #11794, #2569 ) ) ;
#4328=CARTESIAN_POINT ( 'NONE',  ( 20.00000000000000000, 27.00000000000000355, -25.00000000000000000 ) ) ;
#4329=DIRECTION ( 'NONE',  ( 0.000000000000000000, 0.000000000000000000, -1.000000000000000000 ) ) ;
#4344=SHAPE_REPRESENTATION ( 'MirrorHardened Serrated Safety Wedge', ( #11025 ), #6837 ) ;
#4374=PLANE ( 'NONE',  #12974 ) ;
#4392=EDGE_LOOP ( 'NONE', ( #12847, #6527, #12737, #7097 ) ) ;
#4394=DIRECTION ( 'NONE',  ( -0.2425356250363328581, 0.9701425001453318764, 0.000000000000000000 ) ) ;
#4395=CARTESIAN_POINT ( 'NONE',  ( 22.00000000000000000, 70.00000000000000000, -25.00000000000000000 ) ) ;
#4403=VERTEX_POINT ( 'NONE', #681 ) ;
#4409=AXIS2_PLACEMENT_3D ( 'NONE', #13879, #3855, #11897 ) ;
#4420=EDGE_CURVE ( 'NONE', #2086, #6626, #7300, .T. ) ;
#4424=VERTEX_POINT ( 'NONE', #12815 ) ;
#4425=VECTOR ( 'NONE', #3395, 1000.000000000000000 ) ;
#4430=CARTESIAN_POINT ( 'NONE',  ( 54.35294117647056567, -1.411764705882362358, -23.00000000000000000 ) ) ;
#4445=DIRECTION ( 'NONE',  ( 0.000000000000000000, 0.000000000000000000, -1.000000000000000000 ) ) ;
#4450=FACE_OUTER_BOUND ( 'NONE', #3950, .T. ) ;
#4461=ORIENTED_EDGE ( 'NONE', *, *, #10732, .F. ) ;
#4462=EDGE_CURVE ( 'NONE', #1545, #9930, #14282, .T. ) ;
#4470=CARTESIAN_POINT ( 'NONE',  ( 20.00000000000000000, 60.00000000000000711, 25.00000000000000000 ) ) ;
#4482=CARTESIAN_POINT ( 'NONE',  ( 19.99999999999999645, 67.00000000000000000, -25.00000000000000000 ) ) ;
#4513=LINE ( 'NONE', #1327, #1000 ) ;
#4517=EDGE_LOOP ( 'NONE', ( #1710, #3446, #11317, #853 ) ) ;
#4520=CARTESIAN_POINT ( 'NONE',  ( 19.99999999999999645, 57.00000000000000000, 25.00000000000000000 ) ) ;
#4526=ORIENTED_EDGE ( 'NONE', *, *, #9947, .F. ) ;
#4529=EDGE_LOOP ( 'NONE', ( #13408, #7556, #6699, #3004 ) ) ;
#4538=ORIENTED_EDGE ( 'NONE', *, *, #10626, .T. ) ;
#4540=VECTOR ( 'NONE', #9648, 1000.000000000000000 ) ;
#4552=CARTESIAN_POINT ( 'NONE',  ( 57.35294117647057277, -1.411764705882362358, 25.00000000000000000 ) ) ;
#4558=DIRECTION ( 'NONE',  ( -0.2425356250363328581, 0.9701425001453318764, 0.000000000000000000 ) ) ;
#4560=ORIENTED_EDGE ( 'NONE', *, *, #9668, .F. ) ;
#4569=CARTESIAN_POINT ( 'NONE',  ( 20.00000000000000000, 78.00000000000000000, -25.00000000000000000 ) ) ;
#4573=PRODUCT_DEFINITION_CONTEXT ( 'detailed design', #5305, 'design' ) ;
#4584=DIRECTION ( 'NONE',  ( 1.000000000000000000, 0.000000000000000000, -0.000000000000000000 ) ) ;
#4597=ORIENTED_EDGE ( 'NONE', *, *, #1244, .T. ) ;
#4613=DIRECTION ( 'NONE',  ( -0.2425356250363328581, 0.9701425001453318764, 0.000000000000000000 ) ) ;
#4628=CIRCLE ( 'NONE', #1830, 2.100000000000000977 ) ;
#4635=VECTOR ( 'NONE', #4650, 1000.000000000000114 ) ;
#4650=DIRECTION ( 'NONE',  ( -0.2425356250363328581, 0.9701425001453318764, 0.000000000000000000 ) ) ;
#4651=DIRECTION ( 'NONE',  ( 0.000000000000000000, 1.000000000000000000, 0.000000000000000000 ) ) ;
#4667=VECTOR ( 'NONE', #134, 1000.000000000000000 ) ;
#4682=LINE ( 'NONE', #9200, #8961 ) ;
#4691=DIRECTION ( 'NONE',  ( 0.000000000000000000, 1.000000000000000000, 0.000000000000000000 ) ) ;
#4704=STYLED_ITEM ( 'NONE', ( #5314 ), #11715 ) ;
#4712=AXIS2_PLACEMENT_3D ( 'NONE', #6706, #12283, #10154 ) ;
#4715=PLANE ( 'NONE',  #3607 ) ;
#4721=DIRECTION ( 'NONE',  ( 1.000000000000000000, 0.000000000000000000, 0.000000000000000000 ) ) ;
#4723=( NAMED_UNIT ( * ) SI_UNIT ( $, .STERADIAN. ) SOLID_ANGLE_UNIT ( ) );
#4761=FACE_OUTER_BOUND ( 'NONE', #5259, .T. ) ;
#4776=ORIENTED_EDGE ( 'NONE', *, *, #53, .T. ) ;
#4778=CARTESIAN_POINT ( 'NONE',  ( 60.00000000000000000, -6.123233995736768255E-16, -25.00000000000000000 ) ) ;
#4783=LINE ( 'NONE', #13658, #7540 ) ;
#4784=ORIENTED_EDGE ( 'NONE', *, *, #6220, .F. ) ;
#4813=CARTESIAN_POINT ( 'NONE',  ( 20.00000000000000000, 60.00000000000000711, -25.00000000000000000 ) ) ;
#4820=CARTESIAN_POINT ( 'NONE',  ( 20.00000000000000000, 70.00000000000000000, -25.00000000000000000 ) ) ;
#4837=EDGE_LOOP ( 'NONE', ( #1430, #7776, #7577, #3372 ) ) ;
#4839=CARTESIAN_POINT ( 'NONE',  ( 60.00000000000000000, -6.123233995736768255E-16, 25.00000000000000000 ) ) ;
#4854=( LENGTH_UNIT ( ) NAMED_UNIT ( * ) SI_UNIT ( .MILLI., .METRE. ) );
#4859=CARTESIAN_POINT ( 'NONE',  ( 20.00000000000000355, 30.00000000000000711, 25.00000000000000000 ) ) ;
#4864=EDGE_CURVE ( 'NONE', #10880, #12702, #512, .T. ) ;
#4894=DIRECTION ( 'NONE',  ( 1.000000000000000000, 0.000000000000000000, 0.000000000000000000 ) ) ;
#4923=DIRECTION ( 'NONE',  ( 0.000000000000000000, 1.000000000000000000, 0.000000000000000000 ) ) ;
#4924=ORIENTED_EDGE ( 'NONE', *, *, #5928, .T. ) ;
#4932=VECTOR ( 'NONE', #14440, 1000.000000000000000 ) ;
#4936=EDGE_CURVE ( 'NONE', #11358, #6890, #5585, .T. ) ;
#4939=EDGE_CURVE ( 'NONE', #6876, #14018, #3417, .T. ) ;
#4943=LINE ( 'NONE', #5949, #11951 ) ;
#4967=LINE ( 'NONE', #9281, #7699 ) ;
#4977=AXIS2_PLACEMENT_3D ( 'NONE', #5710, #5646, #4445 ) ;
#4978=PRODUCT_DEFINITION_SHAPE ( 'NONE', 'NONE',  #13230 ) ;
#4981=ORIENTED_EDGE ( 'NONE', *, *, #12899, .F. ) ;
#4983=EDGE_LOOP ( 'NONE', ( #7915, #10383, #9231, #8076 ) ) ;
#4998=LINE ( 'NONE', #4778, #11028 ) ;
#5021=ORIENTED_EDGE ( 'NONE', *, *, #5248, .F. ) ;
#5029=CARTESIAN_POINT ( 'NONE',  ( 20.00000000000000000, -5.510910596163090344E-15, 25.00000000000000000 ) ) ;
#5030=DIRECTION ( 'NONE',  ( -1.000000000000000000, 0.000000000000000000, 0.000000000000000000 ) ) ;
#5033=DIRECTION ( 'NONE',  ( 1.000000000000000000, 0.000000000000000000, 0.000000000000000000 ) ) ;
#5034=CARTESIAN_POINT ( 'NONE',  ( 22.00000000000000000, 60.00000000000000711, -25.00000000000000000 ) ) ;
#5046=AXIS2_PLACEMENT_3D ( 'NONE', #7159, #3895, #12983 ) ;
#5048=CARTESIAN_POINT ( 'NONE',  ( 22.00000000000000711, 20.00000000000000355, -25.00000000000000000 ) ) ;
#5057=VERTEX_POINT ( 'NONE', #13873 ) ;
#5062=EDGE_CURVE ( 'NONE', #13646, #7747, #13796, .T. ) ;
#5063=DIRECTION ( 'NONE',  ( -0.2425356250363328581, 0.9701425001453318764, 0.000000000000000000 ) ) ;
#5083=VECTOR ( 'NONE', #11824, 1000.000000000000000 ) ;
#5089=DIRECTION ( 'NONE',  ( 0.000000000000000000, 0.000000000000000000, 1.000000000000000000 ) ) ;
#5093=DIRECTION ( 'NONE',  ( 0.000000000000000000, 0.000000000000000000, 1.000000000000000000 ) ) ;
#5108=LINE ( 'NONE', #4031, #3512 ) ;
#5136=EDGE_LOOP ( 'NONE', ( #4597, #6236, #9716, #14210 ) ) ;
#5174=ORIENTED_EDGE ( 'NONE', *, *, #2234, .T. ) ;
#5175=EDGE_CURVE ( 'NONE', #4153, #6300, #3182, .T. ) ;
#5184=LINE ( 'NONE', #9652, #2331 ) ;
#5197=DIRECTION ( 'NONE',  ( -0.000000000000000000, -0.000000000000000000, 1.000000000000000000 ) ) ;
#5199=VERTEX_POINT ( 'NONE', #10786 ) ;
#5221=LINE ( 'NONE', #9467, #3996 ) ;
#5226=DIRECTION ( 'NONE',  ( 0.000000000000000000, 0.000000000000000000, -1.000000000000000000 ) ) ;
#5231=CARTESIAN_POINT ( 'NONE',  ( 22.00000000000000355, 30.00000000000000711, 25.00000000000000000 ) ) ;
#5248=EDGE_CURVE ( 'NONE', #1545, #950, #10713, .T. ) ;
#5259=EDGE_LOOP ( 'NONE', ( #9666, #6496, #10416, #10841 ) ) ;
#5305=APPLICATION_CONTEXT ( 'automotive_design' ) ;
#5314=PRESENTATION_STYLE_ASSIGNMENT (( #5589 ) ) ;
#5318=AXIS2_PLACEMENT_3D ( 'NONE', #12935, #6249, #706 ) ;
#5336=ORIENTED_EDGE ( 'NONE', *, *, #3581, .T. ) ;
#5339=DIRECTION ( 'NONE',  ( 0.000000000000000000, 1.000000000000000000, 0.000000000000000000 ) ) ;
#5340=ORIENTED_EDGE ( 'NONE', *, *, #5062, .F. ) ;
#5355=VECTOR ( 'NONE', #13607, 1000.000000000000000 ) ;
#5362=SURFACE_STYLE_FILL_AREA ( #13145 ) ;
#5369=ORIENTED_EDGE ( 'NONE', *, *, #13087, .F. ) ;
#5372=EDGE_LOOP ( 'NONE', ( #11122, #9946, #8180, #13050 ) ) ;
#5374=DIRECTION ( 'NONE',  ( 0.000000000000000000, 0.000000000000000000, -1.000000000000000000 ) ) ;
#5377=FACE_OUTER_BOUND ( 'NONE', #7800, .T. ) ;
#5392=EDGE_CURVE ( 'NONE', #13612, #9296, #4967, .T. ) ;
#5399=DIRECTION ( 'NONE',  ( 1.000000000000000000, 0.000000000000000000, 0.000000000000000000 ) ) ;
#5403=PLANE ( 'NONE',  #4028 ) ;
#5412=CARTESIAN_POINT ( 'NONE',  ( 20.00000000000000355, 50.00000000000000000, -25.00000000000000000 ) ) ;
#5436=DIRECTION ( 'NONE',  ( 0.000000000000000000, 0.000000000000000000, 1.000000000000000000 ) ) ;
#5441=DIRECTION ( 'NONE',  ( 1.000000000000000000, 0.000000000000000000, 0.000000000000000000 ) ) ;
#5448=CARTESIAN_POINT ( 'NONE',  ( 20.00000000000000000, 27.00000000000000355, -25.00000000000000000 ) ) ;
#5453=LINE ( 'NONE', #10873, #14206 ) ;
#5456=SURFACE_SIDE_STYLE ('',( #3141 ) ) ;
#5461=ORIENTED_EDGE ( 'NONE', *, *, #8753, .T. ) ;
#5482=VERTEX_POINT ( 'NONE', #9507 ) ;
#5484=DIRECTION ( 'NONE',  ( -0.2425356250363328581, 0.9701425001453318764, 0.000000000000000000 ) ) ;
#5487=EDGE_LOOP ( 'NONE', ( #13801, #4538, #272, #5553, #2751, #5649, #7641, #428, #12183, #578, #8339, #128 ) ) ;
#5496=CARTESIAN_POINT ( 'NONE',  ( 22.00000000000000355, 50.00000000000000000, 25.00000000000000000 ) ) ;
#5502=CARTESIAN_POINT ( 'NONE',  ( 20.00000000000000000, 37.00000000000000711, -25.00000000000000000 ) ) ;
#5513=LINE ( 'NONE', #3259, #8334 ) ;
#5517=VERTEX_POINT ( 'NONE', #9787 ) ;
#5525=ADVANCED_FACE ( 'NONE', ( #7305 ), #14261, .F. ) ;
#5541=EDGE_CURVE ( 'NONE', #9296, #7346, #5184, .T. ) ;
#5542=EDGE_CURVE ( 'NONE', #535, #3862, #8690, .T. ) ;
#5552=EDGE_CURVE ( 'NONE', #7346, #9008, #5108, .T. ) ;
#5553=ORIENTED_EDGE ( 'NONE', *, *, #11256, .F. ) ;
#5570=EDGE_CURVE ( 'NONE', #3442, #10880, #13527, .T. ) ;
#5574=APPLICATION_CONTEXT ( 'automotive_design' ) ;
#5585=LINE ( 'NONE', #10058, #2530 ) ;
#5587=LINE ( 'NONE', #9167, #8117 ) ;
#5589=SURFACE_STYLE_USAGE ( .BOTH. , #5456 ) ;
#5593=VECTOR ( 'NONE', #4558, 1000.000000000000227 ) ;
#5597=ORIENTED_EDGE ( 'NONE', *, *, #6493, .F. ) ;
#5610=LINE ( 'NONE', #1013, #12433 ) ;
#5611=AXIS2_PLACEMENT_3D ( 'NONE', #2169, #11087, #11222 ) ;
#5619=DIRECTION ( 'NONE',  ( 0.000000000000000000, 0.000000000000000000, -1.000000000000000000 ) ) ;
#5629=CARTESIAN_POINT ( 'NONE',  ( 28.00000000000000355, 29.99999999999999645, 25.00000000000000000 ) ) ;
#5630=ORIENTED_EDGE ( 'NONE', *, *, #2575, .T. ) ;
#5633=AXIS2_PLACEMENT_3D ( 'NONE', #2263, #13467, #8980 ) ;
#5634=LINE ( 'NONE', #7832, #7769 ) ;
#5643=DIRECTION ( 'NONE',  ( 1.000000000000000000, 1.224646799147353454E-16, 0.000000000000000000 ) ) ;
#5646=DIRECTION ( 'NONE',  ( 0.000000000000000000, 1.000000000000000000, 0.000000000000000000 ) ) ;
#5649=ORIENTED_EDGE ( 'NONE', *, *, #13995, .T. ) ;
#5651=CARTESIAN_POINT ( 'NONE',  ( 20.00000000000000000, -5.510910596163090344E-15, -25.00000000000000000 ) ) ;
#5652=LINE ( 'NONE', #7784, #1687 ) ;
#5659=VECTOR ( 'NONE', #5484, 1000.000000000000114 ) ;
#5671=ORIENTED_EDGE ( 'NONE', *, *, #163, .F. ) ;
#5683=CARTESIAN_POINT ( 'NONE',  ( 20.00000000000000711, 20.00000000000000355, -25.00000000000000000 ) ) ;
#5710=CARTESIAN_POINT ( 'NONE',  ( 20.00000000000000355, 17.00000000000000000, -25.00000000000000000 ) ) ;
#5726=ORIENTED_EDGE ( 'NONE', *, *, #13402, .F. ) ;
#5729=CARTESIAN_POINT ( 'NONE',  ( 22.00000000000000000, 57.00000000000000000, -25.00000000000000000 ) ) ;
#5731=DIRECTION ( 'NONE',  ( -1.000000000000000000, 0.000000000000000000, 0.000000000000000000 ) ) ;
#5732=CARTESIAN_POINT ( 'NONE',  ( 22.00000000000000355, 37.00000000000000711, -25.00000000000000000 ) ) ;
#5746=DIRECTION ( 'NONE',  ( 0.000000000000000000, 0.000000000000000000, 1.000000000000000000 ) ) ;
#5747=VECTOR ( 'NONE', #5936, 1000.000000000000227 ) ;
#5767=DIRECTION ( 'NONE',  ( 0.000000000000000000, 0.000000000000000000, 1.000000000000000000 ) ) ;
#5787=DIRECTION ( 'NONE',  ( -0.000000000000000000, -1.000000000000000000, 0.000000000000000000 ) ) ;
#5790=DIRECTION ( 'NONE',  ( -1.000000000000000000, -1.224646799147353454E-16, 0.000000000000000000 ) ) ;
#5822=CARTESIAN_POINT ( 'NONE',  ( 33.99999999999998579, 80.00000000000000000, -25.00000000000000000 ) ) ;
#5850=DIRECTION ( 'NONE',  ( -1.000000000000000000, 0.000000000000000000, 0.000000000000000000 ) ) ;
#5854=VECTOR ( 'NONE', #10893, 1000.000000000000000 ) ;
#5855=PLANE ( 'NONE',  #12714 ) ;
#5883=VECTOR ( 'NONE', #11483, 1000.000000000000000 ) ;
#5893=CARTESIAN_POINT ( 'NONE',  ( 20.00000000000000000, 47.00000000000000000, -25.00000000000000000 ) ) ;
#5904=VECTOR ( 'NONE', #5063, 1000.000000000000114 ) ;
#5916=VERTEX_POINT ( 'NONE', #13294 ) ;
#5918=VECTOR ( 'NONE', #6103, 1000.000000000000000 ) ;
#5922=PLANE ( 'NONE',  #4712 ) ;
#5925=DIRECTION ( 'NONE',  ( 0.000000000000000000, 0.000000000000000000, -1.000000000000000000 ) ) ;
#5928=EDGE_CURVE ( 'NONE', #10936, #6145, #6535, .T. ) ;
#5936=DIRECTION ( 'NONE',  ( -0.2425356250363328581, 0.9701425001453318764, 0.000000000000000000 ) ) ;
#5941=EDGE_LOOP ( 'NONE', ( #3079, #4114, #527 ) ) ;
#5942=LINE ( 'NONE', #4859, #12830 ) ;
#5949=CARTESIAN_POINT ( 'NONE',  ( 20.00000000000000355, 50.00000000000000000, -25.00000000000000000 ) ) ;
#5956=DIRECTION ( 'NONE',  ( -0.000000000000000000, -1.000000000000000000, 0.000000000000000000 ) ) ;
#5964=FACE_OUTER_BOUND ( 'NONE', #2201, .T. ) ;
#5976=ADVANCED_FACE ( 'NONE', ( #5377 ), #12187, .T. ) ;
#5986=ORIENTED_EDGE ( 'NONE', *, *, #5570, .F. ) ;
#5992=ORIENTED_EDGE ( 'NONE', *, *, #12112, .F. ) ;
#5998=ORIENTED_EDGE ( 'NONE', *, *, #3562, .F. ) ;
#6002=DIRECTION ( 'NONE',  ( 0.000000000000000000, 0.000000000000000000, -1.000000000000000000 ) ) ;
#6004=VECTOR ( 'NONE', #5643, 1000.000000000000000 ) ;
#6025=ORIENTED_EDGE ( 'NONE', *, *, #14175, .F. ) ;
#6026=DIRECTION ( 'NONE',  ( -1.000000000000000000, 0.000000000000000000, 0.000000000000000000 ) ) ;
#6042=ORIENTED_EDGE ( 'NONE', *, *, #12325, .T. ) ;
#6049=VECTOR ( 'NONE', #11030, 1000.000000000000000 ) ;
#6076=DIRECTION ( 'NONE',  ( 0.8571673007021134438, -1.049727191138620051E-16, 0.5150380749100522682 ) ) ;
#6089=ORIENTED_EDGE ( 'NONE', *, *, #2855, .F. ) ;
#6103=DIRECTION ( 'NONE',  ( -0.000000000000000000, -1.000000000000000000, 0.000000000000000000 ) ) ;
#6111=ORIENTED_EDGE ( 'NONE', *, *, #10316, .F. ) ;
#6124=VERTEX_POINT ( 'NONE', #10344 ) ;
#6144=ORIENTED_EDGE ( 'NONE', *, *, #6681, .F. ) ;
#6145=VERTEX_POINT ( 'NONE', #7182 ) ;
#6155=FACE_OUTER_BOUND ( 'NONE', #13042, .T. ) ;
#6176=CLOSED_SHELL ( 'NONE', ( #10978, #12062, #3109, #12265, #8909, #8610, #9701, #6875, #1005, #973, #7384, #2339, #659, #7125, #14415, #1403, #6908, #7606, #13524, #13823, #6942, #9994, #1059, #1633, #7836, #95, #12394, #30, #12467, #765, #4285, #520, #849, #12463, #484, #5976, #7077, #11371, #6892, #11365, #96, #8875, #2976, #5525 ) ) ;
#6177=ORIENTED_EDGE ( 'NONE', *, *, #1612, .T. ) ;
#6178=PLANE ( 'NONE',  #4409 ) ;
#6190=ORIENTED_EDGE ( 'NONE', *, *, #9080, .T. ) ;
#6200=FACE_OUTER_BOUND ( 'NONE', #4203, .T. ) ;
#6202=EDGE_CURVE ( 'NONE', #5199, #1084, #5221, .T. ) ;
#6203=EDGE_LOOP ( 'NONE', ( #5336, #3635 ) ) ;
#6211=DIRECTION ( 'NONE',  ( -1.000000000000000000, 0.000000000000000000, 0.000000000000000000 ) ) ;
#6218=ORIENTED_EDGE ( 'NONE', *, *, #3876, .F. ) ;
#6220=EDGE_CURVE ( 'NONE', #9772, #3097, #13275, .T. ) ;
#6231=VECTOR ( 'NONE', #1186, 1000.000000000000000 ) ;
#6236=ORIENTED_EDGE ( 'NONE', *, *, #13087, .T. ) ;
#6246=LINE ( 'NONE', #8521, #5083 ) ;
#6247=PLANE ( 'NONE',  #7755 ) ;
#6249=DIRECTION ( 'NONE',  ( 1.000000000000000000, 0.000000000000000000, -0.000000000000000000 ) ) ;
#6251=AXIS2_PLACEMENT_3D ( 'NONE', #10117, #9077, #5925 ) ;
#6279=DIRECTION ( 'NONE',  ( 0.000000000000000000, 0.000000000000000000, 1.000000000000000000 ) ) ;
#6284=ORIENTED_EDGE ( 'NONE', *, *, #5175, .T. ) ;
#6300=VERTEX_POINT ( 'NONE', #4292 ) ;
#6311=CARTESIAN_POINT ( 'NONE',  ( 20.00000000000000000, 60.00000000000000711, -25.00000000000000000 ) ) ;
#6314=ORIENTED_EDGE ( 'NONE', *, *, #6633, .F. ) ;
#6325=CARTESIAN_POINT ( 'NONE',  ( 40.00000000000000711, 80.00000000000000000, 25.00000000000000000 ) ) ;
#6330=CARTESIAN_POINT ( 'NONE',  ( 20.00000000000000355, 17.00000000000000000, -25.00000000000000000 ) ) ;
#6336=DIRECTION ( 'NONE',  ( 1.000000000000000000, 0.000000000000000000, 0.000000000000000000 ) ) ;
#6340=VECTOR ( 'NONE', #1906, 1000.000000000000000 ) ;
#6349=CARTESIAN_POINT ( 'NONE',  ( 20.00000000000000000, 80.00000000000000000, 25.00000000000000000 ) ) ;
#6412=EDGE_LOOP ( 'NONE', ( #13282, #5461, #11058, #4784 ) ) ;
#6413=CARTESIAN_POINT ( 'NONE',  ( 24.99999999999999289, -4.898587196589414604E-15, -25.00000000000000000 ) ) ;
#6431=LINE ( 'NONE', #12081, #8667 ) ;
#6460=ORIENTED_EDGE ( 'NONE', *, *, #1546, .T. ) ;
#6481=AXIS2_PLACEMENT_3D ( 'NONE', #14082, #3977, #4061 ) ;
#6493=EDGE_CURVE ( 'NONE', #5199, #2483, #3467, .T. ) ;
#6494=EDGE_CURVE ( 'NONE', #13612, #6124, #1530, .T. ) ;
#6496=ORIENTED_EDGE ( 'NONE', *, *, #1938, .T. ) ;
#6501=LINE ( 'NONE', #9886, #11235 ) ;
#6510=CARTESIAN_POINT ( 'NONE',  ( 20.00000000000000711, 20.00000000000000355, -25.00000000000000000 ) ) ;
#6520=( LENGTH_UNIT ( ) NAMED_UNIT ( * ) SI_UNIT ( .MILLI., .METRE. ) );
#6522=ORIENTED_EDGE ( 'NONE', *, *, #13271, .F. ) ;
#6524=DIRECTION ( 'NONE',  ( 0.000000000000000000, 0.000000000000000000, 1.000000000000000000 ) ) ;
#6527=ORIENTED_EDGE ( 'NONE', *, *, #13995, .F. ) ;
#6535=LINE ( 'NONE', #3198, #489 ) ;
#6541=EDGE_LOOP ( 'NONE', ( #1455, #9982, #10857, #2955 ) ) ;
#6547=VECTOR ( 'NONE', #9873, 1000.000000000000000 ) ;
#6573=FACE_OUTER_BOUND ( 'NONE', #1570, .T. ) ;
#6581=CIRCLE ( 'NONE', #8205, 2.100000000000000977 ) ;
#6583=ORIENTED_EDGE ( 'NONE', *, *, #6494, .F. ) ;
#6586=ORIENTED_EDGE ( 'NONE', *, *, #6493, .T. ) ;
#6592=AXIS2_PLACEMENT_3D ( 'NONE', #4196, #3098, #7528 ) ;
#6596=EDGE_CURVE ( 'NONE', #11965, #13646, #14061, .T. ) ;
#6605=ORIENTED_EDGE ( 'NONE', *, *, #6596, .T. ) ;
#6613=CARTESIAN_POINT ( 'NONE',  ( 54.35294117647056567, -1.411764705882362358, 23.00000000000000000 ) ) ;
#6617=CARTESIAN_POINT ( 'NONE',  ( 33.99999999999998579, 80.00000000000000000, -23.00000000000000000 ) ) ;
#6618=EDGE_LOOP ( 'NONE', ( #9153, #3839, #7471, #13395 ) ) ;
#6626=VERTEX_POINT ( 'NONE', #7648 ) ;
#6627=AXIS2_PLACEMENT_3D ( 'NONE', #1129, #4584, #2167 ) ;
#6632=CARTESIAN_POINT ( 'NONE',  ( 56.99999999999997868, -8.673617379884035472E-16, -25.00000000000000000 ) ) ;
#6633=EDGE_CURVE ( 'NONE', #13484, #10880, #13462, .T. ) ;
#6646=ORIENTED_EDGE ( 'NONE', *, *, #10847, .T. ) ;
#6662=LINE ( 'NONE', #4430, #13184 ) ;
#6681=EDGE_CURVE ( 'NONE', #9296, #2995, #7874, .T. ) ;
#6685=LINE ( 'NONE', #13578, #3101 ) ;
#6698=DIRECTION ( 'NONE',  ( 0.000000000000000000, 0.000000000000000000, 1.000000000000000000 ) ) ;
#6699=ORIENTED_EDGE ( 'NONE', *, *, #3581, .F. ) ;
#6700=CARTESIAN_POINT ( 'NONE',  ( 54.35294117647056567, -1.411764705882362358, -25.00000000000000000 ) ) ;
#6704=CARTESIAN_POINT ( 'NONE',  ( 30.10000000000000497, 29.99999999999999645, 6.999999999999992006 ) ) ;
#6706=CARTESIAN_POINT ( 'NONE',  ( 54.35294117647056567, -1.411764705882362358, 25.00000000000000000 ) ) ;
#6749=DIRECTION ( 'NONE',  ( -0.000000000000000000, -1.000000000000000000, 0.000000000000000000 ) ) ;
#6778=EDGE_CURVE ( 'NONE', #3711, #4424, #1516, .T. ) ;
#6800=PLANE ( 'NONE',  #14190 ) ;
#6808=VECTOR ( 'NONE', #6934, 1000.000000000000000 ) ;
#6810=DIRECTION ( 'NONE',  ( 0.000000000000000000, 0.000000000000000000, 1.000000000000000000 ) ) ;
#6819=CIRCLE ( 'NONE', #11029, 2.100000000000000977 ) ;
#6837=( GEOMETRIC_REPRESENTATION_CONTEXT ( 3 ) GLOBAL_UNCERTAINTY_ASSIGNED_CONTEXT ( ( #3687 ) ) GLOBAL_UNIT_ASSIGNED_CONTEXT ( ( #4854, #10918, #12099 ) ) REPRESENTATION_CONTEXT ( 'NONE', 'WORKASPACE' ) );
#6871=FACE_OUTER_BOUND ( 'NONE', #87, .T. ) ;
#6874=CARTESIAN_POINT ( 'NONE',  ( 22.00000000000000355, 50.00000000000000000, -25.00000000000000000 ) ) ;
#6875=ADVANCED_FACE ( 'NONE', ( #11765 ), #12949, .F. ) ;
#6876=VERTEX_POINT ( 'NONE', #9635 ) ;
#6886=LINE ( 'NONE', #4839, #6004 ) ;
#6890=VERTEX_POINT ( 'NONE', #1811 ) ;
#6892=ADVANCED_FACE ( 'NONE', ( #8461 ), #7959, .F. ) ;
#6908=ADVANCED_FACE ( 'NONE', ( #6573 ), #13329, .T. ) ;
#6931=AXIS2_PLACEMENT_3D ( 'NONE', #11580, #1559, #8922 ) ;
#6934=DIRECTION ( 'NONE',  ( 0.000000000000000000, 0.000000000000000000, 1.000000000000000000 ) ) ;
#6942=ADVANCED_FACE ( 'NONE', ( #6871 ), #3230, .T. ) ;
#6957=LINE ( 'NONE', #8125, #3831 ) ;
#6958=VERTEX_POINT ( 'NONE', #10093 ) ;
#6975=CARTESIAN_POINT ( 'NONE',  ( 20.00000000000000000, -5.510910596163090344E-15, -25.00000000000000000 ) ) ;
#6986=CARTESIAN_POINT ( 'NONE',  ( 0.000000000000000000, 0.000000000000000000, 25.00000000000000000 ) ) ;
#6993=VECTOR ( 'NONE', #8395, 1000.000000000000000 ) ;
#6998=DIRECTION ( 'NONE',  ( 0.9701425001453319874, 0.2425356250363328858, 0.000000000000000000 ) ) ;
#7014=MECHANICAL_DESIGN_GEOMETRIC_PRESENTATION_REPRESENTATION('',(#4704),#9367);
#7019=FACE_OUTER_BOUND ( 'NONE', #9918, .T. ) ;
#7023=VECTOR ( 'NONE', #4691, 1000.000000000000000 ) ;
#7024=ORIENTED_EDGE ( 'NONE', *, *, #12977, .T. ) ;
#7032=EDGE_CURVE ( 'NONE', #5057, #3097, #11016, .T. ) ;
#7077=ADVANCED_FACE ( 'NONE', ( #996 ), #3423, .F. ) ;
#7093=DIRECTION ( 'NONE',  ( 0.000000000000000000, 0.000000000000000000, -1.000000000000000000 ) ) ;
#7097=ORIENTED_EDGE ( 'NONE', *, *, #3707, .F. ) ;
#7111=CYLINDRICAL_SURFACE ( 'NONE', #6931, 2.100000000000000977 ) ;
#7112=DIRECTION ( 'NONE',  ( 1.000000000000000000, 1.224646799147353454E-16, 0.000000000000000000 ) ) ;
#7125=ADVANCED_FACE ( 'NONE', ( #8751 ), #13805, .F. ) ;
#7142=ORIENTED_EDGE ( 'NONE', *, *, #9080, .F. ) ;
#7159=CARTESIAN_POINT ( 'NONE',  ( 20.00000000000000355, 50.00000000000000000, -25.00000000000000000 ) ) ;
#7177=DIRECTION ( 'NONE',  ( -1.000000000000000000, 0.000000000000000000, 0.000000000000000000 ) ) ;
#7182=CARTESIAN_POINT ( 'NONE',  ( 22.00000000000000000, 70.00000000000000000, -25.00000000000000000 ) ) ;
#7197=CARTESIAN_POINT ( 'NONE',  ( 20.00000000000000000, 37.00000000000000711, -25.00000000000000000 ) ) ;
#7200=DIRECTION ( 'NONE',  ( 0.000000000000000000, 0.000000000000000000, 1.000000000000000000 ) ) ;
#7203=DIRECTION ( 'NONE',  ( 0.000000000000000000, 0.000000000000000000, -1.000000000000000000 ) ) ;
#7206=ORIENTED_EDGE ( 'NONE', *, *, #1040, .T. ) ;
#7215=LINE ( 'NONE', #5034, #9866 ) ;
#7232=EDGE_CURVE ( 'NONE', #7417, #12192, #5942, .T. ) ;
#7249=CARTESIAN_POINT ( 'NONE',  ( 33.99999999999998579, 80.00000000000000000, 25.00000000000000000 ) ) ;
#7252=EDGE_CURVE ( 'NONE', #10823, #3711, #9172, .T. ) ;
#7263=CARTESIAN_POINT ( 'NONE',  ( 40.00000000000000711, 80.00000000000000000, -25.00000000000000000 ) ) ;
#7283=EDGE_CURVE ( 'NONE', #1772, #12392, #6246, .T. ) ;
#7300=CIRCLE ( 'NONE', #6592, 2.000000000000001776 ) ;
#7305=FACE_OUTER_BOUND ( 'NONE', #5941, .T. ) ;
#7311=PRODUCT_CONTEXT ( 'NONE', #5574, 'mechanical' ) ;
#7329=VERTEX_POINT ( 'NONE', #8585 ) ;
#7331=AXIS2_PLACEMENT_3D ( 'NONE', #9488, #8226, #1736 ) ;
#7336=ORIENTED_EDGE ( 'NONE', *, *, #10244, .T. ) ;
#7346=VERTEX_POINT ( 'NONE', #700 ) ;
#7384=ADVANCED_FACE ( 'NONE', ( #7409 ), #6178, .F. ) ;
#7394=LINE ( 'NONE', #7458, #10339 ) ;
#7409=FACE_OUTER_BOUND ( 'NONE', #14417, .T. ) ;
#7410=DIRECTION ( 'NONE',  ( -0.9701425001453319874, -0.2425356250363328858, 0.000000000000000000 ) ) ;
#7417=VERTEX_POINT ( 'NONE', #5231 ) ;
#7429=DIRECTION ( 'NONE',  ( 0.000000000000000000, 0.000000000000000000, -1.000000000000000000 ) ) ;
#7436=DIRECTION ( 'NONE',  ( 0.000000000000000000, 0.000000000000000000, 1.000000000000000000 ) ) ;
#7437=VERTEX_POINT ( 'NONE', #3333 ) ;
#7448=LINE ( 'NONE', #11931, #6340 ) ;
#7449=ORIENTED_EDGE ( 'NONE', *, *, #3800, .T. ) ;
#7458=CARTESIAN_POINT ( 'NONE',  ( 22.00000000000000355, 40.00000000000000711, 25.00000000000000000 ) ) ;
#7469=DIRECTION ( 'NONE',  ( -1.000000000000000000, 0.000000000000000000, 0.000000000000000000 ) ) ;
#7471=ORIENTED_EDGE ( 'NONE', *, *, #6778, .F. ) ;
#7496=AXIS2_PLACEMENT_3D ( 'NONE', #2942, #6279, #9437 ) ;
#7504=ORIENTED_EDGE ( 'NONE', *, *, #10118, .F. ) ;
#7505=VECTOR ( 'NONE', #5089, 1000.000000000000000 ) ;
#7526=PLANE ( 'NONE',  #8039 ) ;
#7528=DIRECTION ( 'NONE',  ( -1.000000000000000000, 0.000000000000000000, 0.000000000000000000 ) ) ;
#7540=VECTOR ( 'NONE', #3689, 1000.000000000000000 ) ;
#7550=DIRECTION ( 'NONE',  ( 0.000000000000000000, -1.000000000000000000, 0.000000000000000000 ) ) ;
#7556=ORIENTED_EDGE ( 'NONE', *, *, #1838, .T. ) ;
#7562=LINE ( 'NONE', #6330, #7505 ) ;
#7572=( LENGTH_UNIT ( ) NAMED_UNIT ( * ) SI_UNIT ( .MILLI., .METRE. ) );
#7577=ORIENTED_EDGE ( 'NONE', *, *, #8108, .F. ) ;
#7579=ORIENTED_EDGE ( 'NONE', *, *, #8753, .F. ) ;
#7581=FACE_BOUND ( 'NONE', #6203, .T. ) ;
#7586=DIRECTION ( 'NONE',  ( 0.000000000000000000, 0.000000000000000000, 1.000000000000000000 ) ) ;
#7606=ADVANCED_FACE ( 'NONE', ( #9010 ), #11422, .T. ) ;
#7620=ORIENTED_EDGE ( 'NONE', *, *, #6681, .T. ) ;
#7621=EDGE_LOOP ( 'NONE', ( #8489, #5630, #545, #2535 ) ) ;
#7632=LINE ( 'NONE', #6617, #11174 ) ;
#7633=EDGE_CURVE ( 'NONE', #10272, #5482, #314, .T. ) ;
#7639=VECTOR ( 'NONE', #12628, 1000.000000000000000 ) ;
#7640=ORIENTED_EDGE ( 'NONE', *, *, #11197, .T. ) ;
#7641=ORIENTED_EDGE ( 'NONE', *, *, #6220, .T. ) ;
#7648=CARTESIAN_POINT ( 'NONE',  ( 22.00000000000000000, 80.00000000000000000, 25.00000000000000000 ) ) ;
#7650=CARTESIAN_POINT ( 'NONE',  ( 20.00000000000000355, 40.00000000000000711, -25.00000000000000000 ) ) ;
#7653=CARTESIAN_POINT ( 'NONE',  ( 56.99999999999997868, -1.031959805901694782E-15, 23.00000000000000000 ) ) ;
#7662=LINE ( 'NONE', #12224, #9924 ) ;
#7675=ORIENTED_EDGE ( 'NONE', *, *, #8384, .T. ) ;
#7679=VECTOR ( 'NONE', #8621, 1000.000000000000000 ) ;
#7683=EDGE_CURVE ( 'NONE', #1123, #9662, #6886, .T. ) ;
#7693=SURFACE_SIDE_STYLE ('',( #5362 ) ) ;
#7699=VECTOR ( 'NONE', #10306, 1000.000000000000000 ) ;
#7701=DIRECTION ( 'NONE',  ( -0.000000000000000000, -1.000000000000000000, 0.000000000000000000 ) ) ;
#7745=VECTOR ( 'NONE', #11176, 1000.000000000000000 ) ;
#7747=VERTEX_POINT ( 'NONE', #8269 ) ;
#7755=AXIS2_PLACEMENT_3D ( 'NONE', #9698, #7410, #703 ) ;
#7769=VECTOR ( 'NONE', #12159, 1000.000000000000000 ) ;
#7776=ORIENTED_EDGE ( 'NONE', *, *, #7793, .T. ) ;
#7784=CARTESIAN_POINT ( 'NONE',  ( 60.00000000000000000, -6.123233995736768255E-16, -25.00000000000000000 ) ) ;
#7789=ORIENTED_EDGE ( 'NONE', *, *, #3599, .T. ) ;
#7793=EDGE_CURVE ( 'NONE', #6124, #12192, #12904, .T. ) ;
#7800=EDGE_LOOP ( 'NONE', ( #4245, #3102, #362, #11340 ) ) ;
#7816=ORIENTED_EDGE ( 'NONE', *, *, #6596, .F. ) ;
#7832=CARTESIAN_POINT ( 'NONE',  ( 20.00000000000000355, 40.00000000000000711, -25.00000000000000000 ) ) ;
#7836=ADVANCED_FACE ( 'NONE', ( #6155 ), #2732, .T. ) ;
#7845=CARTESIAN_POINT ( 'NONE',  ( 20.00000000000000000, 70.00000000000000000, 25.00000000000000000 ) ) ;
#7863=ORIENTED_EDGE ( 'NONE', *, *, #8722, .F. ) ;
#7864=ORIENTED_EDGE ( 'NONE', *, *, #10732, .T. ) ;
#7874=LINE ( 'NONE', #5732, #4667 ) ;
#7879=PLANE ( 'NONE',  #5633 ) ;
#7890=AXIS2_PLACEMENT_3D ( 'NONE', #13965, #10877, #2999 ) ;
#7913=CARTESIAN_POINT ( 'NONE',  ( 20.00000000000000000, 47.00000000000000000, -25.00000000000000000 ) ) ;
#7915=ORIENTED_EDGE ( 'NONE', *, *, #7032, .F. ) ;
#7916=DIRECTION ( 'NONE',  ( -0.2425356250363328581, 0.9701425001453318764, 0.000000000000000000 ) ) ;
#7940=LINE ( 'NONE', #10281, #13198 ) ;
#7959=PLANE ( 'NONE',  #1143 ) ;
#7997=DIRECTION ( 'NONE',  ( 0.000000000000000000, 0.000000000000000000, 1.000000000000000000 ) ) ;
#8000=DIRECTION ( 'NONE',  ( 0.000000000000000000, 0.000000000000000000, 1.000000000000000000 ) ) ;
#8018=CARTESIAN_POINT ( 'NONE',  ( 22.00000000000000355, 37.00000000000000711, -25.00000000000000000 ) ) ;
#8039=AXIS2_PLACEMENT_3D ( 'NONE', #8773, #98, #3301 ) ;
#8071=EDGE_CURVE ( 'NONE', #2483, #4217, #12376, .T. ) ;
#8076=ORIENTED_EDGE ( 'NONE', *, *, #9517, .F. ) ;
#8080=ORIENTED_EDGE ( 'NONE', *, *, #12872, .F. ) ;
#8087=DIRECTION ( 'NONE',  ( 0.000000000000000000, 0.000000000000000000, -1.000000000000000000 ) ) ;
#8108=EDGE_CURVE ( 'NONE', #1573, #12192, #13903, .T. ) ;
#8109=CARTESIAN_POINT ( 'NONE',  ( 20.00000000000000355, 50.00000000000000000, 25.00000000000000000 ) ) ;
#8112=EDGE_LOOP ( 'NONE', ( #1052, #6190, #2295, #127 ) ) ;
#8117=VECTOR ( 'NONE', #4721, 1000.000000000000000 ) ;
#8124=ORIENTED_EDGE ( 'NONE', *, *, #10032, .T. ) ;
#8125=CARTESIAN_POINT ( 'NONE',  ( 12.50000000000002132, 12.49999999999999289, 25.00000000000000000 ) ) ;
#8149=CARTESIAN_POINT ( 'NONE',  ( 20.00000000000000000, 60.00000000000000711, 25.00000000000000000 ) ) ;
#8165=LINE ( 'NONE', #498, #7639 ) ;
#8166=PLANE ( 'NONE',  #8465 ) ;
#8169=ORIENTED_EDGE ( 'NONE', *, *, #2294, .T. ) ;
#8180=ORIENTED_EDGE ( 'NONE', *, *, #2312, .F. ) ;
#8181=ADVANCED_BREP_SHAPE_REPRESENTATION ( '', ( #11715, #11025 ), #6837 ) ;
#8188=CARTESIAN_POINT ( 'NONE',  ( 20.00000000000000000, 27.00000000000000355, 25.00000000000000000 ) ) ;
#8192=CARTESIAN_POINT ( 'NONE',  ( 22.00000000000000355, 47.00000000000000000, 25.00000000000000000 ) ) ;
#8199=VECTOR ( 'NONE', #13989, 1000.000000000000114 ) ;
#8205=AXIS2_PLACEMENT_3D ( 'NONE', #1877, #710, #4231 ) ;
#8223=PLANE ( 'NONE',  #1414 ) ;
#8224=ORIENTED_EDGE ( 'NONE', *, *, #4462, .T. ) ;
#8226=DIRECTION ( 'NONE',  ( 1.000000000000000000, 0.000000000000000000, -0.000000000000000000 ) ) ;
#8227=LINE ( 'NONE', #1655, #11731 ) ;
#8232=PRODUCT ( 'MirrorHardened Serrated Safety Wedge', 'MirrorHardened Serrated Safety Wedge', '', ( #7311 ) ) ;
#8245=LINE ( 'NONE', #12791, #4540 ) ;
#8269=CARTESIAN_POINT ( 'NONE',  ( 22.00000000000000355, 27.00000000000000355, 25.00000000000000000 ) ) ;
#8277=CARTESIAN_POINT ( 'NONE',  ( 20.00000000000000000, 27.00000000000000355, -25.00000000000000000 ) ) ;
#8296=ORIENTED_EDGE ( 'NONE', *, *, #3707, .T. ) ;
#8304=CARTESIAN_POINT ( 'NONE',  ( 22.00000000000000711, 20.00000000000000355, -25.00000000000000000 ) ) ;
#8334=VECTOR ( 'NONE', #7701, 1000.000000000000000 ) ;
#8339=ORIENTED_EDGE ( 'NONE', *, *, #12442, .F. ) ;
#8343=LINE ( 'NONE', #753, #13620 ) ;
#8356=DIRECTION ( 'NONE',  ( 0.000000000000000000, 0.000000000000000000, 1.000000000000000000 ) ) ;
#8378=CARTESIAN_POINT ( 'NONE',  ( 53.99999999999997868, -1.084202172485504434E-15, -25.00000000000000000 ) ) ;
#8384=EDGE_CURVE ( 'NONE', #11506, #25, #261, .T. ) ;
#8386=CARTESIAN_POINT ( 'NONE',  ( 60.00000000000000000, -6.123233995736768255E-16, -25.00000000000000000 ) ) ;
#8394=VERTEX_POINT ( 'NONE', #10500 ) ;
#8395=DIRECTION ( 'NONE',  ( 0.000000000000000000, 0.000000000000000000, 1.000000000000000000 ) ) ;
#8422=COLOUR_RGB ( '', 0.09019608, 0.27058824, 0.51372549) ;
#8425=CARTESIAN_POINT ( 'NONE',  ( 57.35294117647057277, -1.411764705882362358, -25.00000000000000000 ) ) ;
#8447=PLANE ( 'NONE',  #5318 ) ;
#8452=ORIENTED_EDGE ( 'NONE', *, *, #8108, .T. ) ;
#8461=FACE_OUTER_BOUND ( 'NONE', #4983, .T. ) ;
#8465=AXIS2_PLACEMENT_3D ( 'NONE', #4813, #425, #9117 ) ;
#8484=FACE_OUTER_BOUND ( 'NONE', #10475, .T. ) ;
#8485=LINE ( 'NONE', #1901, #1437 ) ;
#8487=CARTESIAN_POINT ( 'NONE',  ( 0.000000000000000000, 0.000000000000000000, 25.00000000000000000 ) ) ;
#8489=ORIENTED_EDGE ( 'NONE', *, *, #12362, .F. ) ;
#8521=CARTESIAN_POINT ( 'NONE',  ( 20.00000000000000000, 5.000000000000000000, -25.00000000000000000 ) ) ;
#8540=CARTESIAN_POINT ( 'NONE',  ( 54.35294117647056567, -1.411764705882362358, 23.00000000000000000 ) ) ;
#8548=ORIENTED_EDGE ( 'NONE', *, *, #3432, .F. ) ;
#8569=DIRECTION ( 'NONE',  ( 0.000000000000000000, 0.000000000000000000, 1.000000000000000000 ) ) ;
#8585=CARTESIAN_POINT ( 'NONE',  ( 25.90000000000000213, 29.99999999999999645, 6.999999999999992006 ) ) ;
#8609=VECTOR ( 'NONE', #43, 1000.000000000000000 ) ;
#8610=ADVANCED_FACE ( 'NONE', ( #4000 ), #8447, .F. ) ;
#8618=VERTEX_POINT ( 'NONE', #1056 ) ;
#8621=DIRECTION ( 'NONE',  ( 0.000000000000000000, 0.000000000000000000, 1.000000000000000000 ) ) ;
#8628=CARTESIAN_POINT ( 'NONE',  ( 54.35294117647056567, -1.411764705882362358, 25.00000000000000000 ) ) ;
#8631=VECTOR ( 'NONE', #12385, 1000.000000000000000 ) ;
#8640=AXIS2_PLACEMENT_3D ( 'NONE', #13177, #10886, #14059 ) ;
#8641=ORIENTED_EDGE ( 'NONE', *, *, #13064, .F. ) ;
#8652=CARTESIAN_POINT ( 'NONE',  ( 20.00000000000000355, 17.00000000000000000, 25.00000000000000000 ) ) ;
#8655=( NAMED_UNIT ( * ) SI_UNIT ( $, .STERADIAN. ) SOLID_ANGLE_UNIT ( ) );
#8663=ORIENTED_EDGE ( 'NONE', *, *, #8384, .F. ) ;
#8667=VECTOR ( 'NONE', #10901, 1000.000000000000000 ) ;
#8669=EDGE_LOOP ( 'NONE', ( #7789, #4229, #5992, #5998 ) ) ;
#8690=LINE ( 'NONE', #1896, #6993 ) ;
#8693=CARTESIAN_POINT ( 'NONE',  ( 22.00000000000000000, 60.00000000000000711, -25.00000000000000000 ) ) ;
#8698=LINE ( 'NONE', #14413, #5854 ) ;
#8704=VECTOR ( 'NONE', #6810, 1000.000000000000000 ) ;
#8722=EDGE_CURVE ( 'NONE', #12012, #12392, #5513, .T. ) ;
#8728=FACE_OUTER_BOUND ( 'NONE', #9677, .T. ) ;
#8729=ORIENTED_EDGE ( 'NONE', *, *, #3562, .T. ) ;
#8741=ORIENTED_EDGE ( 'NONE', *, *, #3599, .F. ) ;
#8751=FACE_OUTER_BOUND ( 'NONE', #4316, .T. ) ;
#8753=EDGE_CURVE ( 'NONE', #2228, #5057, #8165, .T. ) ;
#8761=DIRECTION ( 'NONE',  ( -1.000000000000000000, 0.000000000000000000, 0.000000000000000000 ) ) ;
#8764=FACE_OUTER_BOUND ( 'NONE', #6412, .T. ) ;
#8765=LINE ( 'NONE', #10962, #7745 ) ;
#8773=CARTESIAN_POINT ( 'NONE',  ( 20.00000000000000355, 40.00000000000000711, -25.00000000000000000 ) ) ;
#8797=LINE ( 'NONE', #13279, #3570 ) ;
#8839=DIRECTION ( 'NONE',  ( 0.000000000000000000, -1.000000000000000000, 0.000000000000000000 ) ) ;
#8875=ADVANCED_FACE ( 'NONE', ( #6200 ), #4106, .F. ) ;
#8896=PLANE ( 'NONE',  #12011 ) ;
#8902=VECTOR ( 'NONE', #13478, 1000.000000000000000 ) ;
#8909=ADVANCED_FACE ( 'NONE', ( #14187 ), #11988, .F. ) ;
#8917=ORIENTED_EDGE ( 'NONE', *, *, #607, .F. ) ;
#8922=DIRECTION ( 'NONE',  ( -1.000000000000000000, 0.000000000000000000, 0.000000000000000000 ) ) ;
#8929=AXIS2_PLACEMENT_3D ( 'NONE', #11860, #5197, #4190 ) ;
#8931=DIRECTION ( 'NONE',  ( 0.000000000000000000, 0.000000000000000000, 1.000000000000000000 ) ) ;
#8936=CARTESIAN_POINT ( 'NONE',  ( 19.99999999999999645, 67.00000000000000000, -25.00000000000000000 ) ) ;
#8947=ORIENTED_EDGE ( 'NONE', *, *, #230, .T. ) ;
#8948=PLANE ( 'NONE',  #4977 ) ;
#8949=EDGE_CURVE ( 'NONE', #1753, #1352, #1119, .T. ) ;
#8958=PLANE ( 'NONE',  #12353 ) ;
#8961=VECTOR ( 'NONE', #13691, 1000.000000000000000 ) ;
#8962=VERTEX_POINT ( 'NONE', #8386 ) ;
#8974=DIRECTION ( 'NONE',  ( 0.000000000000000000, 0.000000000000000000, 1.000000000000000000 ) ) ;
#8978=LINE ( 'NONE', #2326, #6547 ) ;
#8980=DIRECTION ( 'NONE',  ( 0.000000000000000000, 0.000000000000000000, -1.000000000000000000 ) ) ;
#8992=CARTESIAN_POINT ( 'NONE',  ( 36.99999999999999289, 80.00000000000000000, -23.00000000000000000 ) ) ;
#9002=LINE ( 'NONE', #13494, #2854 ) ;
#9008=VERTEX_POINT ( 'NONE', #7650 ) ;
#9010=FACE_OUTER_BOUND ( 'NONE', #5372, .T. ) ;
#9020=FACE_OUTER_BOUND ( 'NONE', #6618, .T. ) ;
#9046=CARTESIAN_POINT ( 'NONE',  ( 20.00000000000000000, 5.000000000000000000, -25.00000000000000000 ) ) ;
#9058=LINE ( 'NONE', #11266, #5593 ) ;
#9064=CARTESIAN_POINT ( 'NONE',  ( 22.00000000000000355, 50.00000000000000000, 25.00000000000000000 ) ) ;
#9070=EDGE_CURVE ( 'NONE', #7329, #9244, #4628, .T. ) ;
#9077=DIRECTION ( 'NONE',  ( -1.000000000000000000, 0.000000000000000000, 0.000000000000000000 ) ) ;
#9080=EDGE_CURVE ( 'NONE', #4403, #1350, #3217, .T. ) ;
#9088=DIRECTION ( 'NONE',  ( 0.000000000000000000, 0.000000000000000000, 1.000000000000000000 ) ) ;
#9095=ORIENTED_EDGE ( 'NONE', *, *, #2312, .T. ) ;
#9098=CARTESIAN_POINT ( 'NONE',  ( 19.99999999999999645, 57.00000000000000000, -25.00000000000000000 ) ) ;
#9100=CARTESIAN_POINT ( 'NONE',  ( 20.00000000000000355, 50.00000000000000000, -25.00000000000000000 ) ) ;
#9109=CARTESIAN_POINT ( 'NONE',  ( 33.99999999999998579, 80.00000000000000000, -25.00000000000000000 ) ) ;
#9110=CARTESIAN_POINT ( 'NONE',  ( 20.00000000000000000, 78.00000000000000000, -25.00000000000000000 ) ) ;
#9117=DIRECTION ( 'NONE',  ( 0.000000000000000000, 0.000000000000000000, 1.000000000000000000 ) ) ;
#9137=ORIENTED_EDGE ( 'NONE', *, *, #747, .F. ) ;
#9147=CARTESIAN_POINT ( 'NONE',  ( 22.00000000000000000, 67.00000000000000000, 25.00000000000000000 ) ) ;
#9153=ORIENTED_EDGE ( 'NONE', *, *, #747, .T. ) ;
#9167=CARTESIAN_POINT ( 'NONE',  ( 19.99999999999999645, 67.00000000000000000, -25.00000000000000000 ) ) ;
#9172=LINE ( 'NONE', #9098, #1367 ) ;
#9175=DIRECTION ( 'NONE',  ( -1.000000000000000000, 0.000000000000000000, 0.000000000000000000 ) ) ;
#9180=FACE_OUTER_BOUND ( 'NONE', #9896, .T. ) ;
#9191=CARTESIAN_POINT ( 'NONE',  ( 22.00000000000000355, 50.00000000000000000, -25.00000000000000000 ) ) ;
#9200=CARTESIAN_POINT ( 'NONE',  ( 20.00000000000000000, 70.00000000000000000, -25.00000000000000000 ) ) ;
#9220=EDGE_LOOP ( 'NONE', ( #7620, #7024, #8917, #9754 ) ) ;
#9231=ORIENTED_EDGE ( 'NONE', *, *, #14175, .T. ) ;
#9244=VERTEX_POINT ( 'NONE', #6704 ) ;
#9252=ORIENTED_EDGE ( 'NONE', *, *, #9530, .F. ) ;
#9267=FACE_OUTER_BOUND ( 'NONE', #8112, .T. ) ;
#9279=ORIENTED_EDGE ( 'NONE', *, *, #4936, .F. ) ;
#9280=VERTEX_POINT ( 'NONE', #9110 ) ;
#9281=CARTESIAN_POINT ( 'NONE',  ( 20.00000000000000000, 37.00000000000000711, -25.00000000000000000 ) ) ;
#9285=LINE ( 'NONE', #6874, #6808 ) ;
#9296=VERTEX_POINT ( 'NONE', #8018 ) ;
#9350=ORIENTED_EDGE ( 'NONE', *, *, #1244, .F. ) ;
#9359=LINE ( 'NONE', #10390, #4033 ) ;
#9367=( GEOMETRIC_REPRESENTATION_CONTEXT ( 3 ) GLOBAL_UNCERTAINTY_ASSIGNED_CONTEXT ( ( #14225 ) ) GLOBAL_UNIT_ASSIGNED_CONTEXT ( ( #7572, #9851, #4723 ) ) REPRESENTATION_CONTEXT ( 'NONE', 'WORKASPACE' ) );
#9370=FACE_OUTER_BOUND ( 'NONE', #14070, .T. ) ;
#9378=DIRECTION ( 'NONE',  ( 0.000000000000000000, 0.000000000000000000, 1.000000000000000000 ) ) ;
#9385=AXIS2_PLACEMENT_3D ( 'NONE', #5893, #1444, #8087 ) ;
#9391=LINE ( 'NONE', #7263, #5747 ) ;
#9395=EDGE_CURVE ( 'NONE', #10382, #6124, #11534, .T. ) ;
#9410=COLOUR_RGB ( '', 0.09019608, 0.27058824, 0.51372549) ;
#9437=DIRECTION ( 'NONE',  ( -1.000000000000000000, 0.000000000000000000, 0.000000000000000000 ) ) ;
#9450=CARTESIAN_POINT ( 'NONE',  ( 22.00000000000000000, 67.00000000000000000, -25.00000000000000000 ) ) ;
#9458=CARTESIAN_POINT ( 'NONE',  ( 33.99999999999998579, 80.00000000000000000, 23.00000000000000000 ) ) ;
#9467=CARTESIAN_POINT ( 'NONE',  ( 20.00000000000000000, 47.00000000000000000, -25.00000000000000000 ) ) ;
#9470=ORIENTED_EDGE ( 'NONE', *, *, #1040, .F. ) ;
#9483=ORIENTED_EDGE ( 'NONE', *, *, #11788, .F. ) ;
#9484=CARTESIAN_POINT ( 'NONE',  ( 25.90000000000000213, 29.99999999999999645, 25.00000000000000000 ) ) ;
#9488=CARTESIAN_POINT ( 'NONE',  ( 20.00000000000000000, -5.510910596163090344E-15, -25.00000000000000000 ) ) ;
#9507=CARTESIAN_POINT ( 'NONE',  ( 36.99999999999999289, 80.00000000000000000, 23.00000000000000000 ) ) ;
#9517=EDGE_CURVE ( 'NONE', #3097, #13484, #7632, .T. ) ;
#9528=AXIS2_PLACEMENT_3D ( 'NONE', #2454, #11587, #5790 ) ;
#9530=EDGE_CURVE ( 'NONE', #3255, #7437, #14251, .T. ) ;
#9540=ORIENTED_EDGE ( 'NONE', *, *, #7252, .T. ) ;
#9541=VECTOR ( 'NONE', #5030, 1000.000000000000000 ) ;
#9543=CARTESIAN_POINT ( 'NONE',  ( 60.00000000000000000, -6.123233995736768255E-16, 25.00000000000000000 ) ) ;
#9573=VECTOR ( 'NONE', #800, 1000.000000000000000 ) ;
#9575=EDGE_LOOP ( 'NONE', ( #14117, #10643, #8224, #2131 ) ) ;
#9576=VECTOR ( 'NONE', #5399, 1000.000000000000000 ) ;
#9578=ORIENTED_EDGE ( 'NONE', *, *, #2222, .F. ) ;
#9583=CARTESIAN_POINT ( 'NONE',  ( 20.00000000000000000, 70.00000000000000000, 25.00000000000000000 ) ) ;
#9584=DIRECTION ( 'NONE',  ( -1.000000000000000000, 0.000000000000000000, 0.000000000000000000 ) ) ;
#9592=ORIENTED_EDGE ( 'NONE', *, *, #14087, .F. ) ;
#9604=LINE ( 'NONE', #8425, #5904 ) ;
#9616=CARTESIAN_POINT ( 'NONE',  ( 28.00000000000000355, 29.99999999999999645, 6.999999999999992006 ) ) ;
#9635=CARTESIAN_POINT ( 'NONE',  ( 53.99999999999997868, -1.324077043022348342E-15, 23.00000000000000000 ) ) ;
#9648=DIRECTION ( 'NONE',  ( 0.000000000000000000, 1.000000000000000000, 0.000000000000000000 ) ) ;
#9652=CARTESIAN_POINT ( 'NONE',  ( 22.00000000000000355, 40.00000000000000711, -25.00000000000000000 ) ) ;
#9653=EDGE_CURVE ( 'NONE', #3255, #1772, #1340, .T. ) ;
#9656=LINE ( 'NONE', #9583, #10077 ) ;
#9662=VERTEX_POINT ( 'NONE', #1278 ) ;
#9666=ORIENTED_EDGE ( 'NONE', *, *, #5248, .T. ) ;
#9668=EDGE_CURVE ( 'NONE', #4104, #10936, #5587, .T. ) ;
#9677=EDGE_LOOP ( 'NONE', ( #11795, #12408, #8641, #9592 ) ) ;
#9698=CARTESIAN_POINT ( 'NONE',  ( 40.00000000000000711, 80.00000000000000000, -25.00000000000000000 ) ) ;
#9701=ADVANCED_FACE ( 'NONE', ( #9020 ), #8958, .F. ) ;
#9716=ORIENTED_EDGE ( 'NONE', *, *, #1546, .F. ) ;
#9754=ORIENTED_EDGE ( 'NONE', *, *, #5541, .F. ) ;
#9758=EDGE_CURVE ( 'NONE', #6876, #10272, #3915, .T. ) ;
#9772=VERTEX_POINT ( 'NONE', #11662 ) ;
#9787=CARTESIAN_POINT ( 'NONE',  ( 33.99999999999998579, 80.00000000000000000, 25.00000000000000000 ) ) ;
#9788=LINE ( 'NONE', #4395, #7679 ) ;
#9792=DIRECTION ( 'NONE',  ( -0.8571673007021134438, 0.000000000000000000, 0.5150380749100522682 ) ) ;
#9801=FACE_OUTER_BOUND ( 'NONE', #529, .T. ) ;
#9813=LINE ( 'NONE', #6510, #8704 ) ;
#9814=CARTESIAN_POINT ( 'NONE',  ( 20.00000000000000711, 20.00000000000000355, -25.00000000000000000 ) ) ;
#9851=( NAMED_UNIT ( * ) PLANE_ANGLE_UNIT ( ) SI_UNIT ( $, .RADIAN. ) );
#9866=VECTOR ( 'NONE', #11684, 1000.000000000000000 ) ;
#9869=LINE ( 'NONE', #12208, #14036 ) ;
#9873=DIRECTION ( 'NONE',  ( 1.000000000000000000, 1.224646799147353454E-16, 0.000000000000000000 ) ) ;
#9878=VECTOR ( 'NONE', #4048, 1000.000000000000000 ) ;
#9879=PLANE ( 'NONE',  #10348 ) ;
#9886=CARTESIAN_POINT ( 'NONE',  ( 19.99999999999999645, 57.00000000000000000, -25.00000000000000000 ) ) ;
#9896=EDGE_LOOP ( 'NONE', ( #9540, #13640, #14404, #4461 ) ) ;
#9918=EDGE_LOOP ( 'NONE', ( #33, #11862, #9483, #6089 ) ) ;
#9924=VECTOR ( 'NONE', #10968, 1000.000000000000000 ) ;
#9928=CARTESIAN_POINT ( 'NONE',  ( 54.35294117647056567, -1.411764705882362358, -25.00000000000000000 ) ) ;
#9930=VERTEX_POINT ( 'NONE', #3117 ) ;
#9936=LINE ( 'NONE', #6349, #9573 ) ;
#9946=ORIENTED_EDGE ( 'NONE', *, *, #3432, .T. ) ;
#9947=EDGE_CURVE ( 'NONE', #6958, #3442, #8797, .T. ) ;
#9956=ORIENTED_EDGE ( 'NONE', *, *, #4936, .T. ) ;
#9968=LINE ( 'NONE', #2221, #4932 ) ;
#9982=ORIENTED_EDGE ( 'NONE', *, *, #589, .F. ) ;
#9985=ORIENTED_EDGE ( 'NONE', *, *, #13152, .T. ) ;
#9986=ORIENTED_EDGE ( 'NONE', *, *, #7232, .T. ) ;
#9994=ADVANCED_FACE ( 'NONE', ( #8728 ), #1862, .T. ) ;
#10004=LINE ( 'NONE', #10826, #3732 ) ;
#10011=FACE_OUTER_BOUND ( 'NONE', #9220, .T. ) ;
#10032=EDGE_CURVE ( 'NONE', #9244, #7329, #6819, .T. ) ;
#10058=CARTESIAN_POINT ( 'NONE',  ( 20.00000000000000000, -5.510910596163090344E-15, 25.00000000000000000 ) ) ;
#10065=VECTOR ( 'NONE', #7586, 1000.000000000000000 ) ;
#10077=VECTOR ( 'NONE', #6211, 1000.000000000000000 ) ;
#10093=CARTESIAN_POINT ( 'NONE',  ( 53.99999999999997868, -1.324077043022348342E-15, -23.00000000000000000 ) ) ;
#10096=CARTESIAN_POINT ( 'NONE',  ( 19.99999999999999645, 57.00000000000000000, -25.00000000000000000 ) ) ;
#10117=CARTESIAN_POINT ( 'NONE',  ( 22.00000000000000000, 70.00000000000000000, -25.00000000000000000 ) ) ;
#10118=EDGE_CURVE ( 'NONE', #5057, #6958, #9359, .T. ) ;
#10147=ORIENTED_EDGE ( 'NONE', *, *, #2926, .T. ) ;
#10154=DIRECTION ( 'NONE',  ( 0.2425356250363328581, -0.9701425001453318764, -0.000000000000000000 ) ) ;
#10164=ORIENTED_EDGE ( 'NONE', *, *, #3800, .F. ) ;
#10183=ORIENTED_EDGE ( 'NONE', *, *, #8071, .T. ) ;
#10185=ORIENTED_EDGE ( 'NONE', *, *, #5552, .F. ) ;
#10199=ORIENTED_EDGE ( 'NONE', *, *, #589, .T. ) ;
#10228=EDGE_CURVE ( 'NONE', #4104, #11502, #8698, .T. ) ;
#10244=EDGE_CURVE ( 'NONE', #1954, #13783, #8765, .T. ) ;
#10272=VERTEX_POINT ( 'NONE', #7653 ) ;
#10278=VERTEX_POINT ( 'NONE', #932 ) ;
#10281=CARTESIAN_POINT ( 'NONE',  ( 20.00000000000000000, -5.510910596163090344E-15, 25.00000000000000000 ) ) ;
#10306=DIRECTION ( 'NONE',  ( 1.000000000000000000, 0.000000000000000000, 0.000000000000000000 ) ) ;
#10316=EDGE_CURVE ( 'NONE', #9280, #2086, #4262, .T. ) ;
#10327=VECTOR ( 'NONE', #3269, 1000.000000000000000 ) ;
#10339=VECTOR ( 'NONE', #818, 1000.000000000000000 ) ;
#10344=CARTESIAN_POINT ( 'NONE',  ( 20.00000000000000355, 30.00000000000000711, -25.00000000000000000 ) ) ;
#10348=AXIS2_PLACEMENT_3D ( 'NONE', #12010, #8839, #1085 ) ;
#10382=VERTEX_POINT ( 'NONE', #69 ) ;
#10383=ORIENTED_EDGE ( 'NONE', *, *, #10118, .T. ) ;
#10390=CARTESIAN_POINT ( 'NONE',  ( 60.00000000000000000, -6.123233995736768255E-16, -23.00000000000000000 ) ) ;
#10416=ORIENTED_EDGE ( 'NONE', *, *, #11256, .T. ) ;
#10462=VECTOR ( 'NONE', #9378, 1000.000000000000000 ) ;
#10464=VECTOR ( 'NONE', #11101, 1000.000000000000000 ) ;
#10474=VECTOR ( 'NONE', #5787, 1000.000000000000000 ) ;
#10475=EDGE_LOOP ( 'NONE', ( #2125, #12958, #2015 ) ) ;
#10483=ORIENTED_EDGE ( 'NONE', *, *, #11485, .F. ) ;
#10500=CARTESIAN_POINT ( 'NONE',  ( 20.00000000000000355, 40.00000000000000711, 25.00000000000000000 ) ) ;
#10507=LINE ( 'NONE', #14040, #5918 ) ;
#10579=DIRECTION ( 'NONE',  ( 0.000000000000000000, 0.000000000000000000, 1.000000000000000000 ) ) ;
#10584=ORIENTED_EDGE ( 'NONE', *, *, #5570, .T. ) ;
#10626=EDGE_CURVE ( 'NONE', #14018, #5482, #6431, .T. ) ;
#10627=ORIENTED_EDGE ( 'NONE', *, *, #12007, .T. ) ;
#10643=ORIENTED_EDGE ( 'NONE', *, *, #12899, .T. ) ;
#10659=LINE ( 'NONE', #10803, #1448 ) ;
#10689=LINE ( 'NONE', #14142, #9878 ) ;
#10713=LINE ( 'NONE', #9543, #1626 ) ;
#10732=EDGE_CURVE ( 'NONE', #10823, #535, #6501, .T. ) ;
#10747=ORIENTED_EDGE ( 'NONE', *, *, #3700, .T. ) ;
#10761=ORIENTED_EDGE ( 'NONE', *, *, #13033, .F. ) ;
#10776=ORIENTED_EDGE ( 'NONE', *, *, #12325, .F. ) ;
#10786=CARTESIAN_POINT ( 'NONE',  ( 20.00000000000000000, 47.00000000000000000, -25.00000000000000000 ) ) ;
#10793=ORIENTED_EDGE ( 'NONE', *, *, #11788, .T. ) ;
#10803=CARTESIAN_POINT ( 'NONE',  ( 36.99999999999999289, 80.00000000000000000, 25.00000000000000000 ) ) ;
#10810=EDGE_CURVE ( 'NONE', #9280, #1954, #1460, .T. ) ;
#10823=VERTEX_POINT ( 'NONE', #10096 ) ;
#10826=CARTESIAN_POINT ( 'NONE',  ( 20.00000000000000711, 20.00000000000000355, 25.00000000000000000 ) ) ;
#10834=EDGE_LOOP ( 'NONE', ( #1672, #9985, #5340, #7816 ) ) ;
#10836=PRODUCT_DEFINITION_FORMATION_WITH_SPECIFIED_SOURCE ( 'ANY', '', #8232, .NOT_KNOWN. ) ;
#10841=ORIENTED_EDGE ( 'NONE', *, *, #4462, .F. ) ;
#10847=EDGE_CURVE ( 'NONE', #11506, #13079, #9285, .T. ) ;
#10857=ORIENTED_EDGE ( 'NONE', *, *, #10228, .F. ) ;
#10873=CARTESIAN_POINT ( 'NONE',  ( 53.99999999999997868, -1.347111479062091166E-15, -25.00000000000000000 ) ) ;
#10875=ORIENTED_EDGE ( 'NONE', *, *, #9758, .T. ) ;
#10877=DIRECTION ( 'NONE',  ( 0.000000000000000000, -1.000000000000000000, 0.000000000000000000 ) ) ;
#10880=VERTEX_POINT ( 'NONE', #5822 ) ;
#10886=DIRECTION ( 'NONE',  ( 0.000000000000000000, 0.000000000000000000, 1.000000000000000000 ) ) ;
#10893=DIRECTION ( 'NONE',  ( 0.000000000000000000, 0.000000000000000000, 1.000000000000000000 ) ) ;
#10897=CARTESIAN_POINT ( 'NONE',  ( 20.00000000000000000, 37.00000000000000711, -25.00000000000000000 ) ) ;
#10901=DIRECTION ( 'NONE',  ( 1.000000000000000000, 0.000000000000000000, 0.000000000000000000 ) ) ;
#10911=EDGE_CURVE ( 'NONE', #3032, #13783, #9656, .T. ) ;
#10918=( NAMED_UNIT ( * ) PLANE_ANGLE_UNIT ( ) SI_UNIT ( $, .RADIAN. ) );
#10936=VERTEX_POINT ( 'NONE', #13034 ) ;
#10945=DIRECTION ( 'NONE',  ( -0.2425356250363328581, 0.9701425001453318764, 0.000000000000000000 ) ) ;
#10947=VECTOR ( 'NONE', #10945, 1000.000000000000114 ) ;
#10949=VECTOR ( 'NONE', #3792, 1000.000000000000000 ) ;
#10962=CARTESIAN_POINT ( 'NONE',  ( 20.00000000000000000, 70.00000000000000000, -25.00000000000000000 ) ) ;
#10968=DIRECTION ( 'NONE',  ( 1.000000000000000000, 0.000000000000000000, 0.000000000000000000 ) ) ;
#10978=ADVANCED_FACE ( 'NONE', ( #8484 ), #953, .F. ) ;
#11004=CARTESIAN_POINT ( 'NONE',  ( 40.00000000000000711, 80.00000000000000000, -25.00000000000000000 ) ) ;
#11016=LINE ( 'NONE', #3204, #10947 ) ;
#11025=AXIS2_PLACEMENT_3D ( 'NONE', #167, #6524, #5441 ) ;
#11028=VECTOR ( 'NONE', #13651, 1000.000000000000000 ) ;
#11029=AXIS2_PLACEMENT_3D ( 'NONE', #9616, #5226, #4146 ) ;
#11030=DIRECTION ( 'NONE',  ( 0.000000000000000000, 1.000000000000000000, 0.000000000000000000 ) ) ;
#11058=ORIENTED_EDGE ( 'NONE', *, *, #7032, .T. ) ;
#11084=ORIENTED_EDGE ( 'NONE', *, *, #13988, .F. ) ;
#11087=DIRECTION ( 'NONE',  ( 0.000000000000000000, 0.000000000000000000, 1.000000000000000000 ) ) ;
#11099=DIRECTION ( 'NONE',  ( -0.000000000000000000, -1.000000000000000000, 0.000000000000000000 ) ) ;
#11101=DIRECTION ( 'NONE',  ( -1.000000000000000000, 0.000000000000000000, 0.000000000000000000 ) ) ;
#11114=FACE_OUTER_BOUND ( 'NONE', #4251, .T. ) ;
#11115=ORIENTED_EDGE ( 'NONE', *, *, #5541, .T. ) ;
#11118=CARTESIAN_POINT ( 'NONE',  ( 54.35294117647056567, -1.411764705882362358, -23.00000000000000000 ) ) ;
#11122=ORIENTED_EDGE ( 'NONE', *, *, #1696, .T. ) ;
#11126=CARTESIAN_POINT ( 'NONE',  ( 20.00000000000000355, 17.00000000000000000, -25.00000000000000000 ) ) ;
#11174=VECTOR ( 'NONE', #14185, 1000.000000000000000 ) ;
#11176=DIRECTION ( 'NONE',  ( 0.000000000000000000, 0.000000000000000000, 1.000000000000000000 ) ) ;
#11193=FACE_OUTER_BOUND ( 'NONE', #4529, .T. ) ;
#11197=EDGE_CURVE ( 'NONE', #5916, #11584, #3086, .T. ) ;
#11222=DIRECTION ( 'NONE',  ( -1.000000000000000000, 0.000000000000000000, 0.000000000000000000 ) ) ;
#11235=VECTOR ( 'NONE', #13126, 1000.000000000000000 ) ;
#11252=DIRECTION ( 'NONE',  ( -0.2425356250363328581, 0.9701425001453318764, 0.000000000000000000 ) ) ;
#11256=EDGE_CURVE ( 'NONE', #13670, #9930, #4183, .T. ) ;
#11266=CARTESIAN_POINT ( 'NONE',  ( 40.00000000000000711, 80.00000000000000000, 25.00000000000000000 ) ) ;
#11280=ORIENTED_EDGE ( 'NONE', *, *, #6778, .T. ) ;
#11281=( GEOMETRIC_REPRESENTATION_CONTEXT ( 3 ) GLOBAL_UNCERTAINTY_ASSIGNED_CONTEXT ( ( #1628 ) ) GLOBAL_UNIT_ASSIGNED_CONTEXT ( ( #6520, #1049, #8655 ) ) REPRESENTATION_CONTEXT ( 'NONE', 'WORKASPACE' ) );
#11309=ORIENTED_EDGE ( 'NONE', *, *, #1696, .F. ) ;
#11317=ORIENTED_EDGE ( 'NONE', *, *, #12586, .F. ) ;
#11328=EDGE_CURVE ( 'NONE', #2806, #7329, #8485, .T. ) ;
#11332=DIRECTION ( 'NONE',  ( -1.000000000000000000, 0.000000000000000000, 0.000000000000000000 ) ) ;
#11338=LINE ( 'NONE', #9064, #7023 ) ;
#11340=ORIENTED_EDGE ( 'NONE', *, *, #12442, .T. ) ;
#11358=VERTEX_POINT ( 'NONE', #3290 ) ;
#11365=ADVANCED_FACE ( 'NONE', ( #12134 ), #5922, .F. ) ;
#11371=ADVANCED_FACE ( 'NONE', ( #8764 ), #5403, .F. ) ;
#11387=CARTESIAN_POINT ( 'NONE',  ( 24.99999999999999289, -4.898587196589414604E-15, -25.00000000000000000 ) ) ;
#11408=LINE ( 'NONE', #13771, #12903 ) ;
#11422=PLANE ( 'NONE',  #6251 ) ;
#11429=LINE ( 'NONE', #3844, #1267 ) ;
#11449=ORIENTED_EDGE ( 'NONE', *, *, #3743, .F. ) ;
#11483=DIRECTION ( 'NONE',  ( -1.000000000000000000, 0.000000000000000000, 0.000000000000000000 ) ) ;
#11485=EDGE_CURVE ( 'NONE', #11488, #3442, #8978, .T. ) ;
#11488=VERTEX_POINT ( 'NONE', #11387 ) ;
#11493=ORIENTED_EDGE ( 'NONE', *, *, #2294, .F. ) ;
#11495=CARTESIAN_POINT ( 'NONE',  ( 57.35294117647057277, -1.411764705882362358, 23.00000000000000000 ) ) ;
#11502=VERTEX_POINT ( 'NONE', #12556 ) ;
#11506=VERTEX_POINT ( 'NONE', #9191 ) ;
#11534=LINE ( 'NONE', #3868, #9541 ) ;
#11553=CARTESIAN_POINT ( 'NONE',  ( 20.00000000000000000, -5.510910596163090344E-15, -25.00000000000000000 ) ) ;
#11570=CARTESIAN_POINT ( 'NONE',  ( 20.00000000000000355, 30.00000000000000711, -25.00000000000000000 ) ) ;
#11580=CARTESIAN_POINT ( 'NONE',  ( 28.00000000000000355, 29.99999999999999645, 25.00000000000000000 ) ) ;
#11584=VERTEX_POINT ( 'NONE', #8304 ) ;
#11587=DIRECTION ( 'NONE',  ( -1.224646799147353454E-16, 1.000000000000000000, 0.000000000000000000 ) ) ;
#11597=PLANE ( 'NONE',  #1497 ) ;
#11620=DIRECTION ( 'NONE',  ( -1.000000000000000000, 0.000000000000000000, 0.000000000000000000 ) ) ;
#11653=CARTESIAN_POINT ( 'NONE',  ( 22.00000000000000711, 20.00000000000000355, 25.00000000000000000 ) ) ;
#11662=CARTESIAN_POINT ( 'NONE',  ( 36.99999999999999289, 80.00000000000000000, -25.00000000000000000 ) ) ;
#11675=DIRECTION ( 'NONE',  ( 0.000000000000000000, 1.000000000000000000, 0.000000000000000000 ) ) ;
#11683=CARTESIAN_POINT ( 'NONE',  ( 28.00000000000000355, 29.99999999999999645, 25.00000000000000000 ) ) ;
#11684=DIRECTION ( 'NONE',  ( 0.000000000000000000, 0.000000000000000000, 1.000000000000000000 ) ) ;
#11711=ORIENTED_EDGE ( 'NONE', *, *, #3876, .T. ) ;
#11715=MANIFOLD_SOLID_BREP ( '<Hardened Serrated Safety Wedge>-<AdvancedHole1>', #6176 ) ;
#11731=VECTOR ( 'NONE', #11675, 1000.000000000000000 ) ;
#11741=ORIENTED_EDGE ( 'NONE', *, *, #1838, .F. ) ;
#11765=FACE_OUTER_BOUND ( 'NONE', #5136, .T. ) ;
#11767=ORIENTED_EDGE ( 'NONE', *, *, #7283, .T. ) ;
#11774=VECTOR ( 'NONE', #5850, 1000.000000000000000 ) ;
#11780=DIRECTION ( 'NONE',  ( 0.000000000000000000, 1.000000000000000000, 0.000000000000000000 ) ) ;
#11788=EDGE_CURVE ( 'NONE', #10382, #7417, #13589, .T. ) ;
#11794=ORIENTED_EDGE ( 'NONE', *, *, #9758, .F. ) ;
#11795=ORIENTED_EDGE ( 'NONE', *, *, #13033, .T. ) ;
#11824=DIRECTION ( 'NONE',  ( 0.000000000000000000, 0.000000000000000000, -1.000000000000000000 ) ) ;
#11826=ORIENTED_EDGE ( 'NONE', *, *, #10228, .T. ) ;
#11860=CARTESIAN_POINT ( 'NONE',  ( 22.00000000000000000, 78.00000000000000000, -25.00000000000000000 ) ) ;
#11862=ORIENTED_EDGE ( 'NONE', *, *, #13345, .T. ) ;
#11874=DIRECTION ( 'NONE',  ( -1.000000000000000000, 0.000000000000000000, 0.000000000000000000 ) ) ;
#11878=ORIENTED_EDGE ( 'NONE', *, *, #607, .T. ) ;
#11886=VECTOR ( 'NONE', #2700, 1000.000000000000000 ) ;
#11897=DIRECTION ( 'NONE',  ( -1.000000000000000000, 0.000000000000000000, 0.000000000000000000 ) ) ;
#11906=CARTESIAN_POINT ( 'NONE',  ( 19.99999999999999645, 67.00000000000000000, 25.00000000000000000 ) ) ;
#11917=ORIENTED_EDGE ( 'NONE', *, *, #4152, .T. ) ;
#11931=CARTESIAN_POINT ( 'NONE',  ( 20.00000000000000000, 47.00000000000000000, 25.00000000000000000 ) ) ;
#11951=VECTOR ( 'NONE', #7200, 1000.000000000000000 ) ;
#11965=VERTEX_POINT ( 'NONE', #12304 ) ;
#11972=VECTOR ( 'NONE', #4160, 1000.000000000000000 ) ;
#11978=LINE ( 'NONE', #2920, #11972 ) ;
#11988=PLANE ( 'NONE',  #7890 ) ;
#12004=VECTOR ( 'NONE', #6076, 1000.000000000000000 ) ;
#12007=EDGE_CURVE ( 'NONE', #4217, #13079, #11338, .T. ) ;
#12010=CARTESIAN_POINT ( 'NONE',  ( 20.00000000000000000, 70.00000000000000000, -25.00000000000000000 ) ) ;
#12011=AXIS2_PLACEMENT_3D ( 'NONE', #1148, #13675, #12346 ) ;
#12012=VERTEX_POINT ( 'NONE', #11126 ) ;
#12021=ORIENTED_EDGE ( 'NONE', *, *, #13772, .F. ) ;
#12057=ORIENTED_EDGE ( 'NONE', *, *, #9668, .T. ) ;
#12062=ADVANCED_FACE ( 'NONE', ( #11193 ), #1035, .F. ) ;
#12081=CARTESIAN_POINT ( 'NONE',  ( 33.99999999999998579, 80.00000000000000000, 23.00000000000000000 ) ) ;
#12094=LINE ( 'NONE', #5502, #6231 ) ;
#12099=( NAMED_UNIT ( * ) SI_UNIT ( $, .STERADIAN. ) SOLID_ANGLE_UNIT ( ) );
#12112=EDGE_CURVE ( 'NONE', #5916, #7437, #11408, .T. ) ;
#12134=FACE_OUTER_BOUND ( 'NONE', #7621, .T. ) ;
#12159=DIRECTION ( 'NONE',  ( 0.000000000000000000, 0.000000000000000000, 1.000000000000000000 ) ) ;
#12183=ORIENTED_EDGE ( 'NONE', *, *, #6633, .T. ) ;
#12187=CYLINDRICAL_SURFACE ( 'NONE', #5611, 2.000000000000001776 ) ;
#12192=VERTEX_POINT ( 'NONE', #1605 ) ;
#12199=ORIENTED_EDGE ( 'NONE', *, *, #230, .F. ) ;
#12207=AXIS2_PLACEMENT_3D ( 'NONE', #2006, #7550, #5436 ) ;
#12208=CARTESIAN_POINT ( 'NONE',  ( 20.00000000000000000, -5.510910596163090344E-15, 25.00000000000000000 ) ) ;
#12224=CARTESIAN_POINT ( 'NONE',  ( 20.00000000000000000, 37.00000000000000711, 25.00000000000000000 ) ) ;
#12265=ADVANCED_FACE ( 'NONE', ( #4761 ), #14272, .T. ) ;
#12266=CARTESIAN_POINT ( 'NONE',  ( 22.00000000000000000, 60.00000000000000711, 25.00000000000000000 ) ) ;
#12283=DIRECTION ( 'NONE',  ( -0.9701425001453319874, -0.2425356250363328858, 0.000000000000000000 ) ) ;
#12294=ORIENTED_EDGE ( 'NONE', *, *, #13271, .T. ) ;
#12297=CARTESIAN_POINT ( 'NONE',  ( 22.00000000000000711, 20.00000000000000355, -25.00000000000000000 ) ) ;
#12304=CARTESIAN_POINT ( 'NONE',  ( 20.00000000000000000, 27.00000000000000355, -25.00000000000000000 ) ) ;
#12325=EDGE_CURVE ( 'NONE', #1084, #4217, #7448, .T. ) ;
#12346=DIRECTION ( 'NONE',  ( 0.000000000000000000, 0.000000000000000000, -1.000000000000000000 ) ) ;
#12353=AXIS2_PLACEMENT_3D ( 'NONE', #3489, #3563, #7997 ) ;
#12362=EDGE_CURVE ( 'NONE', #9662, #5517, #4186, .T. ) ;
#12370=FACE_OUTER_BOUND ( 'NONE', #4392, .T. ) ;
#12373=EDGE_CURVE ( 'NONE', #11965, #13624, #3964, .T. ) ;
#12376=LINE ( 'NONE', #1253, #4425 ) ;
#12385=DIRECTION ( 'NONE',  ( -0.000000000000000000, -1.000000000000000000, 0.000000000000000000 ) ) ;
#12392=VERTEX_POINT ( 'NONE', #9046 ) ;
#12394=ADVANCED_FACE ( 'NONE', ( #10011 ), #7879, .T. ) ;
#12408=ORIENTED_EDGE ( 'NONE', *, *, #2222, .T. ) ;
#12417=DIRECTION ( 'NONE',  ( -0.000000000000000000, -1.000000000000000000, 0.000000000000000000 ) ) ;
#12433=VECTOR ( 'NONE', #1231, 1000.000000000000000 ) ;
#12435=EDGE_LOOP ( 'NONE', ( #378, #8080, #10147, #708 ) ) ;
#12442=EDGE_CURVE ( 'NONE', #6626, #12702, #5610, .T. ) ;
#12443=CARTESIAN_POINT ( 'NONE',  ( 22.00000000000000000, 80.00000000000000000, -25.00000000000000000 ) ) ;
#12463=ADVANCED_FACE ( 'NONE', ( #9267 ), #8166, .T. ) ;
#12467=ADVANCED_FACE ( 'NONE', ( #5964 ), #13752, .T. ) ;
#12514=ORIENTED_EDGE ( 'NONE', *, *, #7683, .F. ) ;
#12516=CARTESIAN_POINT ( 'NONE',  ( 20.00000000000000000, 37.00000000000000711, 25.00000000000000000 ) ) ;
#12527=CARTESIAN_POINT ( 'NONE',  ( 20.00000000000000000, 47.00000000000000000, 25.00000000000000000 ) ) ;
#12528=LINE ( 'NONE', #543, #12004 ) ;
#12556=CARTESIAN_POINT ( 'NONE',  ( 19.99999999999999645, 67.00000000000000000, 25.00000000000000000 ) ) ;
#12568=VECTOR ( 'NONE', #7112, 1000.000000000000000 ) ;
#12579=AXIS2_PLACEMENT_3D ( 'NONE', #4482, #212, #13252 ) ;
#12586=EDGE_CURVE ( 'NONE', #4153, #4403, #7215, .T. ) ;
#12628=DIRECTION ( 'NONE',  ( 0.000000000000000000, 0.000000000000000000, 1.000000000000000000 ) ) ;
#12661=VECTOR ( 'NONE', #222, 1000.000000000000000 ) ;
#12670=VECTOR ( 'NONE', #13788, 1000.000000000000000 ) ;
#12702=VERTEX_POINT ( 'NONE', #12443 ) ;
#12714=AXIS2_PLACEMENT_3D ( 'NONE', #8277, #1553, #6002 ) ;
#12733=LINE ( 'NONE', #8109, #5883 ) ;
#12737=ORIENTED_EDGE ( 'NONE', *, *, #2926, .F. ) ;
#12746=LINE ( 'NONE', #1401, #11774 ) ;
#12759=ORIENTED_EDGE ( 'NONE', *, *, #5392, .F. ) ;
#12776=LINE ( 'NONE', #2612, #10949 ) ;
#12791=CARTESIAN_POINT ( 'NONE',  ( 22.00000000000000355, 50.00000000000000000, -25.00000000000000000 ) ) ;
#12815=CARTESIAN_POINT ( 'NONE',  ( 20.00000000000000355, 50.00000000000000000, 25.00000000000000000 ) ) ;
#12816=DIRECTION ( 'NONE',  ( 0.000000000000000000, 0.000000000000000000, 1.000000000000000000 ) ) ;
#12830=VECTOR ( 'NONE', #1281, 1000.000000000000000 ) ;
#12842=ORIENTED_EDGE ( 'NONE', *, *, #10847, .F. ) ;
#12847=ORIENTED_EDGE ( 'NONE', *, *, #14119, .T. ) ;
#12851=FACE_OUTER_BOUND ( 'NONE', #13562, .T. ) ;
#12858=VECTOR ( 'NONE', #4394, 1000.000000000000114 ) ;
#12860=DIRECTION ( 'NONE',  ( 1.000000000000000000, 0.000000000000000000, -0.000000000000000000 ) ) ;
#12871=EDGE_LOOP ( 'NONE', ( #9095, #2980, #13479, #5671 ) ) ;
#12872=EDGE_CURVE ( 'NONE', #8962, #950, #4998, .T. ) ;
#12889=DIRECTION ( 'NONE',  ( 0.000000000000000000, 1.000000000000000000, 0.000000000000000000 ) ) ;
#12899=EDGE_CURVE ( 'NONE', #10272, #1545, #8343, .T. ) ;
#12903=VECTOR ( 'NONE', #2640, 1000.000000000000000 ) ;
#12904=LINE ( 'NONE', #11570, #10462 ) ;
#12910=VECTOR ( 'NONE', #2019, 1000.000000000000000 ) ;
#12930=STYLED_ITEM ( 'NONE', ( #2074 ), #8181 ) ;
#12935=CARTESIAN_POINT ( 'NONE',  ( 20.00000000000000000, -5.510910596163090344E-15, -25.00000000000000000 ) ) ;
#12942=FACE_OUTER_BOUND ( 'NONE', #1874, .T. ) ;
#12943=DIRECTION ( 'NONE',  ( 0.000000000000000000, 0.000000000000000000, 1.000000000000000000 ) ) ;
#12949=PLANE ( 'NONE',  #2545 ) ;
#12958=ORIENTED_EDGE ( 'NONE', *, *, #3769, .T. ) ;
#12965=DIRECTION ( 'NONE',  ( -1.000000000000000000, 0.000000000000000000, 0.000000000000000000 ) ) ;
#12973=DIRECTION ( 'NONE',  ( 0.000000000000000000, 0.000000000000000000, 1.000000000000000000 ) ) ;
#12974=AXIS2_PLACEMENT_3D ( 'NONE', #3132, #2018, #5374 ) ;
#12977=EDGE_CURVE ( 'NONE', #2995, #10278, #7394, .T. ) ;
#12983=DIRECTION ( 'NONE',  ( 0.000000000000000000, 0.000000000000000000, 1.000000000000000000 ) ) ;
#12998=ORIENTED_EDGE ( 'NONE', *, *, #10911, .F. ) ;
#13027=FACE_OUTER_BOUND ( 'NONE', #2440, .T. ) ;
#13033=EDGE_CURVE ( 'NONE', #11584, #8618, #3242, .T. ) ;
#13034=CARTESIAN_POINT ( 'NONE',  ( 22.00000000000000000, 67.00000000000000000, -25.00000000000000000 ) ) ;
#13042=EDGE_LOOP ( 'NONE', ( #10793, #9986, #13619, #13322 ) ) ;
#13050=ORIENTED_EDGE ( 'NONE', *, *, #5928, .F. ) ;
#13064=EDGE_CURVE ( 'NONE', #13624, #6890, #9813, .T. ) ;
#13069=SURFACE_STYLE_USAGE ( .BOTH. , #7693 ) ;
#13079=VERTEX_POINT ( 'NONE', #5496 ) ;
#13081=FACE_OUTER_BOUND ( 'NONE', #4517, .T. ) ;
#13087=EDGE_CURVE ( 'NONE', #9008, #8394, #5634, .T. ) ;
#13111=CARTESIAN_POINT ( 'NONE',  ( 20.00000000000000000, -5.510910596163090344E-15, -25.00000000000000000 ) ) ;
#13126=DIRECTION ( 'NONE',  ( 1.000000000000000000, 0.000000000000000000, 0.000000000000000000 ) ) ;
#13136=AXIS2_PLACEMENT_3D ( 'NONE', #3465, #1260, #7093 ) ;
#13137=DIRECTION ( 'NONE',  ( -0.000000000000000000, -1.000000000000000000, 0.000000000000000000 ) ) ;
#13140=VECTOR ( 'NONE', #9584, 1000.000000000000000 ) ;
#13145=FILL_AREA_STYLE ('',( #14378 ) ) ;
#13152=EDGE_CURVE ( 'NONE', #11358, #7747, #1470, .T. ) ;
#13177=CARTESIAN_POINT ( 'NONE',  ( 28.00000000000000355, 29.99999999999999645, 6.999999999999992006 ) ) ;
#13184=VECTOR ( 'NONE', #2063, 1000.000000000000114 ) ;
#13186=FACE_OUTER_BOUND ( 'NONE', #12871, .T. ) ;
#13198=VECTOR ( 'NONE', #12417, 1000.000000000000000 ) ;
#13202=CARTESIAN_POINT ( 'NONE',  ( 22.00000000000000711, 20.00000000000000355, -25.00000000000000000 ) ) ;
#13230=PRODUCT_DEFINITION ( 'UNKNOWN', '', #10836, #4573 ) ;
#13252=DIRECTION ( 'NONE',  ( 0.000000000000000000, 0.000000000000000000, -1.000000000000000000 ) ) ;
#13257=CARTESIAN_POINT ( 'NONE',  ( 22.00000000000000000, 70.00000000000000000, 25.00000000000000000 ) ) ;
#13271=EDGE_CURVE ( 'NONE', #13079, #4424, #12733, .T. ) ;
#13275=LINE ( 'NONE', #2072, #13583 ) ;
#13279=CARTESIAN_POINT ( 'NONE',  ( 53.99999999999997868, -1.347111479062091166E-15, -25.00000000000000000 ) ) ;
#13282=ORIENTED_EDGE ( 'NONE', *, *, #14119, .F. ) ;
#13286=FACE_OUTER_BOUND ( 'NONE', #8669, .T. ) ;
#13294=CARTESIAN_POINT ( 'NONE',  ( 22.00000000000000711, 17.00000000000000000, -25.00000000000000000 ) ) ;
#13322=ORIENTED_EDGE ( 'NONE', *, *, #9395, .F. ) ;
#13329=PLANE ( 'NONE',  #12579 ) ;
#13345=EDGE_CURVE ( 'NONE', #7747, #7417, #1908, .T. ) ;
#13362=VECTOR ( 'NONE', #13137, 1000.000000000000000 ) ;
#13368=EDGE_CURVE ( 'NONE', #6300, #1350, #10689, .T. ) ;
#13373=CARTESIAN_POINT ( 'NONE',  ( 60.00000000000000000, -6.123233995736768255E-16, 25.00000000000000000 ) ) ;
#13377=DIRECTION ( 'NONE',  ( -0.000000000000000000, -1.000000000000000000, 0.000000000000000000 ) ) ;
#13382=DIRECTION ( 'NONE',  ( 0.2425356250363328581, -0.9701425001453318764, -0.000000000000000000 ) ) ;
#13395=ORIENTED_EDGE ( 'NONE', *, *, #7252, .F. ) ;
#13402=EDGE_CURVE ( 'NONE', #12702, #9280, #760, .T. ) ;
#13408=ORIENTED_EDGE ( 'NONE', *, *, #9070, .T. ) ;
#13415=VECTOR ( 'NONE', #11874, 1000.000000000000000 ) ;
#13417=CARTESIAN_POINT ( 'NONE',  ( 22.00000000000000355, 37.00000000000000711, 25.00000000000000000 ) ) ;
#13462=LINE ( 'NONE', #9109, #5355 ) ;
#13467=DIRECTION ( 'NONE',  ( -1.000000000000000000, 0.000000000000000000, 0.000000000000000000 ) ) ;
#13478=DIRECTION ( 'NONE',  ( -0.000000000000000000, -1.000000000000000000, 0.000000000000000000 ) ) ;
#13479=ORIENTED_EDGE ( 'NONE', *, *, #10244, .F. ) ;
#13483=DIRECTION ( 'NONE',  ( 0.000000000000000000, 0.000000000000000000, 1.000000000000000000 ) ) ;
#13484=VERTEX_POINT ( 'NONE', #2199 ) ;
#13486=CARTESIAN_POINT ( 'NONE',  ( 20.00000000000000000, -5.510910596163090344E-15, 25.00000000000000000 ) ) ;
#13494=CARTESIAN_POINT ( 'NONE',  ( 40.00000000000000711, 80.00000000000000000, -25.00000000000000000 ) ) ;
#13506=PLANE ( 'NONE',  #6627 ) ;
#13524=ADVANCED_FACE ( 'NONE', ( #13186 ), #9879, .T. ) ;
#13526=ORIENTED_EDGE ( 'NONE', *, *, #12112, .T. ) ;
#13527=LINE ( 'NONE', #6700, #12858 ) ;
#13562=EDGE_LOOP ( 'NONE', ( #3264, #8741, #637, #608 ) ) ;
#13578=CARTESIAN_POINT ( 'NONE',  ( 25.90000000000000213, 29.99999999999999645, 25.00000000000000000 ) ) ;
#13583=VECTOR ( 'NONE', #3114, 1000.000000000000000 ) ;
#13589=LINE ( 'NONE', #120, #1410 ) ;
#13590=ORIENTED_EDGE ( 'NONE', *, *, #12872, .T. ) ;
#13607=DIRECTION ( 'NONE',  ( 0.000000000000000000, 0.000000000000000000, -1.000000000000000000 ) ) ;
#13612=VERTEX_POINT ( 'NONE', #7197 ) ;
#13619=ORIENTED_EDGE ( 'NONE', *, *, #7793, .F. ) ;
#13620=VECTOR ( 'NONE', #8569, 1000.000000000000000 ) ;
#13623=PLANE ( 'NONE',  #1512 ) ;
#13624=VERTEX_POINT ( 'NONE', #5683 ) ;
#13640=ORIENTED_EDGE ( 'NONE', *, *, #2475, .T. ) ;
#13646=VERTEX_POINT ( 'NONE', #2681 ) ;
#13651=DIRECTION ( 'NONE',  ( 0.000000000000000000, 0.000000000000000000, 1.000000000000000000 ) ) ;
#13658=CARTESIAN_POINT ( 'NONE',  ( 24.99999999999999289, -4.898587196589414604E-15, -25.00000000000000000 ) ) ;
#13668=DIRECTION ( 'NONE',  ( 0.000000000000000000, 0.000000000000000000, 1.000000000000000000 ) ) ;
#13670=VERTEX_POINT ( 'NONE', #6325 ) ;
#13673=ORIENTED_EDGE ( 'NONE', *, *, #2264, .T. ) ;
#13675=DIRECTION ( 'NONE',  ( 0.000000000000000000, 1.000000000000000000, 0.000000000000000000 ) ) ;
#13677=AXIS2_PLACEMENT_3D ( 'NONE', #10897, #5339, #940 ) ;
#13691=DIRECTION ( 'NONE',  ( -1.000000000000000000, 0.000000000000000000, 0.000000000000000000 ) ) ;
#13697=EDGE_LOOP ( 'NONE', ( #6025, #2668, #10584, #6314 ) ) ;
#13752=PLANE ( 'NONE',  #9385 ) ;
#13762=VECTOR ( 'NONE', #6336, 1000.000000000000000 ) ;
#13771=CARTESIAN_POINT ( 'NONE',  ( 22.00000000000000711, 17.00000000000000000, -25.00000000000000000 ) ) ;
#13772=EDGE_CURVE ( 'NONE', #4104, #6300, #4513, .T. ) ;
#13783=VERTEX_POINT ( 'NONE', #7845 ) ;
#13788=DIRECTION ( 'NONE',  ( 0.000000000000000000, 0.000000000000000000, -1.000000000000000000 ) ) ;
#13790=VECTOR ( 'NONE', #4894, 1000.000000000000000 ) ;
#13793=CARTESIAN_POINT ( 'NONE',  ( 24.99999999999999289, -4.898587196589414604E-15, 25.00000000000000000 ) ) ;
#13796=LINE ( 'NONE', #547, #606 ) ;
#13800=CARTESIAN_POINT ( 'NONE',  ( 60.00000000000000000, -6.123233995736768255E-16, 23.00000000000000000 ) ) ;
#13801=ORIENTED_EDGE ( 'NONE', *, *, #13933, .T. ) ;
#13805=PLANE ( 'NONE',  #9528 ) ;
#13823=ADVANCED_FACE ( 'NONE', ( #13286 ), #8948, .T. ) ;
#13840=CARTESIAN_POINT ( 'NONE',  ( 20.00000000000000000, 78.00000000000000000, 25.00000000000000000 ) ) ;
#13846=DIRECTION ( 'NONE',  ( -1.000000000000000000, -1.224646799147353454E-16, 0.000000000000000000 ) ) ;
#13853=PLANE ( 'NONE',  #5046 ) ;
#13866=MECHANICAL_DESIGN_GEOMETRIC_PRESENTATION_REPRESENTATION('',(#12930),#11281);
#13867=LINE ( 'NONE', #7249, #12670 ) ;
#13873=CARTESIAN_POINT ( 'NONE',  ( 56.99999999999997868, -8.673617379884035472E-16, -23.00000000000000000 ) ) ;
#13879=CARTESIAN_POINT ( 'NONE',  ( 0.000000000000000000, 0.000000000000000000, -25.00000000000000000 ) ) ;
#13903=LINE ( 'NONE', #13486, #11886 ) ;
#13905=ORIENTED_EDGE ( 'NONE', *, *, #1612, .F. ) ;
#13933=EDGE_CURVE ( 'NONE', #5517, #14018, #13867, .T. ) ;
#13965=CARTESIAN_POINT ( 'NONE',  ( 20.00000000000000000, 80.00000000000000000, -25.00000000000000000 ) ) ;
#13988=EDGE_CURVE ( 'NONE', #1123, #1772, #6957, .T. ) ;
#13989=DIRECTION ( 'NONE',  ( -0.2425356250363328581, 0.9701425001453318764, 0.000000000000000000 ) ) ;
#13995=EDGE_CURVE ( 'NONE', #3669, #9772, #12746, .T. ) ;
#14018=VERTEX_POINT ( 'NONE', #9458 ) ;
#14036=VECTOR ( 'NONE', #11099, 1000.000000000000000 ) ;
#14040=CARTESIAN_POINT ( 'NONE',  ( 20.00000000000000000, -5.510910596163090344E-15, -25.00000000000000000 ) ) ;
#14059=DIRECTION ( 'NONE',  ( -1.000000000000000000, 0.000000000000000000, 0.000000000000000000 ) ) ;
#14061=LINE ( 'NONE', #4328, #9576 ) ;
#14070=EDGE_LOOP ( 'NONE', ( #6646, #12294, #4066, #8663 ) ) ;
#14071=VECTOR ( 'NONE', #1831, 1000.000000000000000 ) ;
#14075=LINE ( 'NONE', #9450, #3547 ) ;
#14082=CARTESIAN_POINT ( 'NONE',  ( 20.00000000000000355, 30.00000000000000711, -25.00000000000000000 ) ) ;
#14087=EDGE_CURVE ( 'NONE', #11584, #13624, #3980, .T. ) ;
#14093=DIRECTION ( 'NONE',  ( 0.000000000000000000, 0.000000000000000000, 1.000000000000000000 ) ) ;
#14109=ORIENTED_EDGE ( 'NONE', *, *, #13345, .F. ) ;
#14117=ORIENTED_EDGE ( 'NONE', *, *, #7633, .F. ) ;
#14119=EDGE_CURVE ( 'NONE', #2228, #9772, #9604, .T. ) ;
#14142=CARTESIAN_POINT ( 'NONE',  ( 20.00000000000000000, 60.00000000000000711, -25.00000000000000000 ) ) ;
#14148=CARTESIAN_POINT ( 'NONE',  ( 30.10000000000000497, 29.99999999999999645, 25.00000000000000000 ) ) ;
#14175=EDGE_CURVE ( 'NONE', #6958, #13484, #6662, .T. ) ;
#14185=DIRECTION ( 'NONE',  ( -1.000000000000000000, 0.000000000000000000, 0.000000000000000000 ) ) ;
#14187=FACE_OUTER_BOUND ( 'NONE', #5487, .T. ) ;
#14190=AXIS2_PLACEMENT_3D ( 'NONE', #2342, #14093, #7177 ) ;
#14194=ORIENTED_EDGE ( 'NONE', *, *, #2836, .F. ) ;
#14206=VECTOR ( 'NONE', #4314, 1000.000000000000000 ) ;
#14210=ORIENTED_EDGE ( 'NONE', *, *, #6202, .F. ) ;
#14213=VECTOR ( 'NONE', #9175, 1000.000000000000000 ) ;
#14215=DIRECTION ( 'NONE',  ( 0.000000000000000000, 0.000000000000000000, 1.000000000000000000 ) ) ;
#14225=UNCERTAINTY_MEASURE_WITH_UNIT (LENGTH_MEASURE( 1.000000000000000082E-05 ), #7572, 'distance_accuracy_value', 'NONE');
#14226=LINE ( 'NONE', #2000, #13362 ) ;
#14249=CARTESIAN_POINT ( 'NONE',  ( 20.00000000000000000, 80.00000000000000000, -25.00000000000000000 ) ) ;
#14251=LINE ( 'NONE', #913, #13762 ) ;
#14261=CONICAL_SURFACE ( 'NONE', #8640, 2.100000000000000977, 1.029744258676656754 ) ;
#14272=PLANE ( 'NONE',  #3556 ) ;
#14282=LINE ( 'NONE', #2128, #5659 ) ;
#14302=AXIS2_PLACEMENT_3D ( 'NONE', #5629, #13483, #1250 ) ;
#14304=SHAPE_REPRESENTATION_RELATIONSHIP ( 'NONE' , 'NONE' ,  #4344, #8181 ) ;
#14308=FACE_OUTER_BOUND ( 'NONE', #12435, .T. ) ;
#14326=VECTOR ( 'NONE', #12889, 1000.000000000000000 ) ;
#14338=FACE_OUTER_BOUND ( 'NONE', #2911, .T. ) ;
#14378=FILL_AREA_STYLE_COLOUR ( '', #9410 ) ;
#14404=ORIENTED_EDGE ( 'NONE', *, *, #5542, .F. ) ;
#14413=CARTESIAN_POINT ( 'NONE',  ( 19.99999999999999645, 67.00000000000000000, -25.00000000000000000 ) ) ;
#14415=ADVANCED_FACE ( 'NONE', ( #14308 ), #6247, .F. ) ;
#14417=EDGE_LOOP ( 'NONE', ( #10483, #10164, #7863, #8729, #7640, #3147, #3593, #6605, #3410, #4110, #6583, #851, #11115, #4161, #9350, #6586, #8947, #7675, #9137, #7864, #13673, #6284, #12021, #12057, #4924, #1764, #1347, #5726, #2526, #5986 ) ) ;
#14425=LINE ( 'NONE', #2129, #3745 ) ;
#14440=DIRECTION ( 'NONE',  ( -0.000000000000000000, -1.000000000000000000, 0.000000000000000000 ) ) ;
ENDSEC;
END-ISO-10303-21;
